ISO-10303-21;
HEADER;
FILE_DESCRIPTION (('STEP AP214'),
    '1' );
FILE_NAME ('domed cap nut_din_DIN 1587 - M4 --NNU.step',
    '2026-10-08T05:45:04',
    ( '' ),
    ( '' ),
    'SwSTEP 2.0',
    'SolidWorks 2026',
    '' );
FILE_SCHEMA (( 'AUTOMOTIVE_DESIGN' ));
ENDSEC;

DATA;
#8=CARTESIAN_POINT ( 'NONE',  ( 3.200000000000000178, 2.020725942163657862, -3.499999999999999556 ) ) ;
#10=FACE_OUTER_BOUND ( 'NONE', #392, .T. ) ;
#26=CARTESIAN_POINT ( 'NONE',  ( 4.750000000000000888, 3.249999999999998668, 0.000000000000000000 ) ) ;
#36=AXIS2_PLACEMENT_3D ( 'NONE', #5242, #7853, #1848 ) ;
#41=DIRECTION ( 'NONE',  ( 1.000000000000000000, 0.000000000000000000, 0.000000000000000000 ) ) ;
#42=SURFACE_SIDE_STYLE ('',( #5116 ) ) ;
#50=DIRECTION ( 'NONE',  ( 0.000000000000000000, 0.000000000000000000, -1.000000000000000000 ) ) ;
#58=VERTEX_POINT ( 'NONE', #781 ) ;
#64=CARTESIAN_POINT ( 'NONE',  ( 0.1388410611045408360, -2.351840044243144856, 2.926493552095781325 ) ) ;
#82=EDGE_LOOP ( 'NONE', ( #7039, #8451, #8267 ) ) ;
#95=ORIENTED_EDGE ( 'NONE', *, *, #9906, .F. ) ;
#97=DIRECTION ( 'NONE',  ( 1.000000000000000000, -0.000000000000000000, -0.000000000000000000 ) ) ;
#105=CARTESIAN_POINT ( 'NONE',  ( 6.876213465810407786E-15, -3.202582148906756299, -1.452965002680407514 ) ) ;
#131=EDGE_CURVE ( 'NONE', #6804, #8565, #10133, .T. ) ;
#135=CONICAL_SURFACE ( 'NONE', #3683, 4.624785217660733139, 1.047197551196604071 ) ;
#141=CARTESIAN_POINT ( 'NONE',  ( 0.000000000000000000, 0.000000000000000000, 0.000000000000000000 ) ) ;
#152=AXIS2_PLACEMENT_3D ( 'NONE', #3028, #4590, #5417 ) ;
#158=EDGE_CURVE ( 'NONE', #2901, #3727, #5085, .T. ) ;
#165=ADVANCED_FACE ( 'NONE', ( #10 ), #10244, .T. ) ;
#172=ORIENTED_EDGE ( 'NONE', *, *, #2907, .T. ) ;
#181=CARTESIAN_POINT ( 'NONE',  ( 4.750000000000000888, -1.622657008870242882E-15, 0.000000000000000000 ) ) ;
#201=CARTESIAN_POINT ( 'NONE',  ( 0.000000000000000000, 3.980102097228895766E-16, -3.249999999999998224 ) ) ;
#205=DIRECTION ( 'NONE',  ( 1.000000000000000000, 0.000000000000000000, 0.000000000000000000 ) ) ;
#255=DIRECTION ( 'NONE',  ( -1.000000000000000000, -0.000000000000000000, -0.000000000000000000 ) ) ;
#262=PLANE ( 'NONE',  #4144 ) ;
#278=ORIENTED_EDGE ( 'NONE', *, *, #1388, .F. ) ;
#308=AXIS2_PLACEMENT_3D ( 'NONE', #6956, #4296, #9565 ) ;
#332=ORIENTED_EDGE ( 'NONE', *, *, #981, .F. ) ;
#344=CARTESIAN_POINT ( 'NONE',  ( 0.2949799022107380542, 1.977804580622975611E-16, -1.615000000000000213 ) ) ;
#345=CARTESIAN_POINT ( 'NONE',  ( 0.2704726383733979667, 0.000000000000000000, 0.000000000000000000 ) ) ;
#365=ORIENTED_EDGE ( 'NONE', *, *, #5871, .F. ) ;
#392=EDGE_LOOP ( 'NONE', ( #6819, #3302, #6878, #5552 ) ) ;
#395=DIRECTION ( 'NONE',  ( 0.000000000000000000, 0.000000000000000000, -1.000000000000000000 ) ) ;
#400=DIRECTION ( 'NONE',  ( -1.000000000000000000, -0.000000000000000000, -0.000000000000000000 ) ) ;
#401=( LENGTH_UNIT ( ) NAMED_UNIT ( * ) SI_UNIT ( .MILLI., .METRE. ) );
#403=CARTESIAN_POINT ( 'NONE',  ( 4.800000000000000711, 2.020667218593132755E-16, -1.649999999999999911 ) ) ;
#419=EDGE_LOOP ( 'NONE', ( #2323, #566, #3009, #4097 ) ) ;
#428=CARTESIAN_POINT ( 'NONE',  ( 2.887392608830845031, -2.020725942164465661, -3.499999999999999556 ) ) ;
#432=CARTESIAN_POINT ( 'NONE',  ( 0.1381424733900992741, -1.355358988605521287, 3.500000000000000000 ) ) ;
#438=AXIS2_PLACEMENT_3D ( 'NONE', #345, #1017, #4528 ) ;
#442=CARTESIAN_POINT ( 'NONE',  ( 0.1381424733901099877, -1.355358988605575687, -3.500000000000000000 ) ) ;
#452=DIRECTION ( 'NONE',  ( 0.000000000000000000, 0.000000000000000000, -1.000000000000000000 ) ) ;
#461=ORIENTED_EDGE ( 'NONE', *, *, #4163, .T. ) ;
#476=COLOUR_RGB ( '', 0.09019608, 0.27058824, 0.51372549) ;
#488=ADVANCED_FACE ( 'NONE', ( #4064 ), #713, .F. ) ;
#520=CARTESIAN_POINT ( 'NONE',  ( 2.887392608830372964, -2.020725942163647648, 3.499999999999999556 ) ) ;
#532=CARTESIAN_POINT ( 'NONE',  ( 3.200000000000000178, 2.020725942163657862, -3.499999999999999556 ) ) ;
#556=FACE_OUTER_BOUND ( 'NONE', #1467, .T. ) ;
#566=ORIENTED_EDGE ( 'NONE', *, *, #2127, .T. ) ;
#582=B_SPLINE_CURVE_WITH_KNOTS ( 'NONE', 3,
 ( #6456, #10019, #1519, #4189 ),
 .UNSPECIFIED., .F., .F.,
 ( 4, 4 ),
 ( 2.380739282169293681E-07, 0.002044882221487522803 ),
 .UNSPECIFIED. ) ;
#588=CARTESIAN_POINT ( 'NONE',  ( 3.199999999999999734, -3.031088913245550298, -1.749999999999972911 ) ) ;
#601=CARTESIAN_POINT ( 'NONE',  ( -4.235164736271498614E-18, -0.3416191432522799887, -3.499999999999999556 ) ) ;
#608=ADVANCED_FACE ( 'NONE', ( #7733 ), #3443, .T. ) ;
#611=AXIS2_PLACEMENT_3D ( 'NONE', #141, #10257, #7591 ) ;
#617=CONICAL_SURFACE ( 'NONE', #6842, 4.624785217660733139, 1.047197551196604071 ) ;
#623=EDGE_CURVE ( 'NONE', #6258, #6815, #9271, .T. ) ;
#626=CIRCLE ( 'NONE', #6313, 1.650000000000000355 ) ;
#639=ORIENTED_EDGE ( 'NONE', *, *, #10746, .T. ) ;
#665=CARTESIAN_POINT ( 'NONE',  ( 3.199999999999999734, 0.000000000000000000, -3.499999999999999556 ) ) ;
#685=EDGE_CURVE ( 'NONE', #8160, #10068, #10693, .T. ) ;
#702=VERTEX_POINT ( 'NONE', #6220 ) ;
#708=CARTESIAN_POINT ( 'NONE',  ( 2.550604951803072673, 0.000000000000000000, 0.000000000000000000 ) ) ;
#713=PLANE ( 'NONE',  #1157 ) ;
#714=CARTESIAN_POINT ( 'NONE',  ( 3.060260095956253146, 1.362955318038518771, -3.500000000000000000 ) ) ;
#755=CARTESIAN_POINT ( 'NONE',  ( 2.982310868301981888, -1.691919446222082568, -3.499999999999999556 ) ) ;
#778=AXIS2_PLACEMENT_3D ( 'NONE', #10087, #5202, #962 ) ;
#781=CARTESIAN_POINT ( 'NONE',  ( 3.200000000000000178, 0.000000000000000000, -3.369999999999997886 ) ) ;
#783=VERTEX_POINT ( 'NONE', #2849 ) ;
#790=CIRCLE ( 'NONE', #2794, 3.499999999999997780 ) ;
#791=AXIS2_PLACEMENT_3D ( 'NONE', #5616, #9047, #3159 ) ;
#804=AXIS2_PLACEMENT_3D ( 'NONE', #846, #4248, #10016 ) ;
#834=VECTOR ( 'NONE', #10059, 999.9999999999998863 ) ;
#846=CARTESIAN_POINT ( 'NONE',  ( 3.200000000000000178, 2.020725942163738686, 3.499999999999999556 ) ) ;
#850=ORIENTED_EDGE ( 'NONE', *, *, #2068, .F. ) ;
#851=AXIS2_PLACEMENT_3D ( 'NONE', #2764, #4948, #10873 ) ;
#853=B_SPLINE_CURVE_WITH_KNOTS ( 'NONE', 3,
 ( #2831, #6202, #1987, #5374, #8758, #1473 ),
 .UNSPECIFIED., .F., .F.,
 ( 4, 2, 4 ),
 ( 0.002044882221487568340, 0.003063384235218514964, 0.004081886248949461587 ),
 .UNSPECIFIED. ) ;
#876=PRESENTATION_STYLE_ASSIGNMENT (( #5720 ) ) ;
#886=DIRECTION ( 'NONE',  ( 0.000000000000000000, 1.224646799147355672E-16, 1.000000000000000000 ) ) ;
#889=ORIENTED_EDGE ( 'NONE', *, *, #4930, .T. ) ;
#895=DIRECTION ( 'NONE',  ( 0.000000000000000000, 0.000000000000000000, 1.000000000000000000 ) ) ;
#899=PLANE ( 'NONE',  #3125 ) ;
#901=DIRECTION ( 'NONE',  ( 1.000000000000000000, 0.000000000000000000, 0.000000000000000000 ) ) ;
#913=CARTESIAN_POINT ( 'NONE',  ( 2.887392608830347207, 2.020725942163738686, 3.499999999999999556 ) ) ;
#915=ADVANCED_FACE ( 'NONE', ( #5337 ), #6104, .F. ) ;
#928=ORIENTED_EDGE ( 'NONE', *, *, #4667, .T. ) ;
#947=VERTEX_POINT ( 'NONE', #7894 ) ;
#956=DIRECTION ( 'NONE',  ( 0.000000000000000000, 0.000000000000000000, -1.000000000000000000 ) ) ;
#962=DIRECTION ( 'NONE',  ( 0.000000000000000000, 0.000000000000000000, -1.000000000000000000 ) ) ;
#968=CARTESIAN_POINT ( 'NONE',  ( 2.550604951803072673, 0.000000000000000000, 0.000000000000000000 ) ) ;
#981=EDGE_CURVE ( 'NONE', #3105, #4377, #2174, .T. ) ;
#986=ORIENTED_EDGE ( 'NONE', *, *, #3897, .F. ) ;
#991=CARTESIAN_POINT ( 'NONE',  ( 3.061158938895386150, 3.710337782248038341, -0.5735064479040072882 ) ) ;
#995=DIRECTION ( 'NONE',  ( 1.000000000000000000, -0.000000000000000000, -0.000000000000000000 ) ) ;
#1005=ADVANCED_FACE ( 'NONE', ( #10335 ), #4662, .F. ) ;
#1013=CARTESIAN_POINT ( 'NONE',  ( 3.200000000000000178, 0.000000000000000000, 0.000000000000000000 ) ) ;
#1017=DIRECTION ( 'NONE',  ( 1.000000000000000000, -0.000000000000000000, -0.000000000000000000 ) ) ;
#1027=ORIENTED_EDGE ( 'NONE', *, *, #5671, .F. ) ;
#1031=AXIS2_PLACEMENT_3D ( 'NONE', #968, #6031, #7704 ) ;
#1070=DIRECTION ( 'NONE',  ( -0.5735764363510461594, 1.003171929053524747E-16, -0.8191520442889916875 ) ) ;
#1155=AXIS2_PLACEMENT_3D ( 'NONE', #9102, #8072, #452 ) ;
#1157=AXIS2_PLACEMENT_3D ( 'NONE', #10837, #3223, #1349 ) ;
#1160=EDGE_LOOP ( 'NONE', ( #461, #9264, #6541, #1917, #7943, #7067 ) ) ;
#1164=CARTESIAN_POINT ( 'NONE',  ( 0.3126073911691312213, -2.020725942164384836, 3.499999999999999556 ) ) ;
#1178=ORIENTED_EDGE ( 'NONE', *, *, #6407, .F. ) ;
#1185=CARTESIAN_POINT ( 'NONE',  ( 0.2704726383733979667, 2.234980408443919708E-16, -1.650000000000000355 ) ) ;
#1187=CARTESIAN_POINT ( 'NONE',  ( 0.1397399040437575513, 1.362955318038573838, 3.499999999999998224 ) ) ;
#1211=AXIS2_PLACEMENT_3D ( 'NONE', #5865, #5096, #7646 ) ;
#1227=CARTESIAN_POINT ( 'NONE',  ( 0.02937408083519319271, -0.6808742863896684039, 3.500000000000000000 ) ) ;
#1244=CARTESIAN_POINT ( 'NONE',  ( 2.887392608830349428, 4.041451884327400101, -2.289061810243902218E-14 ) ) ;
#1256=ADVANCED_FACE ( 'NONE', ( #2665 ), #8657, .F. ) ;
#1262=EDGE_CURVE ( 'NONE', #6109, #2863, #8240, .T. ) ;
#1265=CARTESIAN_POINT ( 'NONE',  ( 3.200000000000000178, 3.031088913245510774, -1.750000000000042411 ) ) ;
#1269=FACE_OUTER_BOUND ( 'NONE', #1160, .T. ) ;
#1276=CONICAL_SURFACE ( 'NONE', #4993, 1664.279482350528269, 1.029744258676657198 ) ;
#1319=CYLINDRICAL_SURFACE ( 'NONE', #7171, 1.650000000000000355 ) ;
#1341=CIRCLE ( 'NONE', #10414, 2.000000000000000000 ) ;
#1343=FACE_OUTER_BOUND ( 'NONE', #2659, .T. ) ;
#1349=DIRECTION ( 'NONE',  ( 0.000000000000000000, 0.4999999999999921729, -0.8660254037844431485 ) ) ;
#1352=ORIENTED_EDGE ( 'NONE', *, *, #8934, .F. ) ;
#1380=EDGE_CURVE ( 'NONE', #10134, #4348, #10599, .T. ) ;
#1388=EDGE_CURVE ( 'NONE', #8904, #8565, #9707, .T. ) ;
#1392=ORIENTED_EDGE ( 'NONE', *, *, #1408, .F. ) ;
#1408=EDGE_CURVE ( 'NONE', #10875, #10068, #10636, .T. ) ;
#1412=CARTESIAN_POINT ( 'NONE',  ( 3.200000000000000178, 3.031088913245510774, -1.750000000000042411 ) ) ;
#1418=DIRECTION ( 'NONE',  ( 0.000000000000000000, 0.000000000000000000, 1.000000000000000000 ) ) ;
#1426=CARTESIAN_POINT ( 'NONE',  ( 3.200000000000000178, -0.3416191432521806237, 3.499999999999999112 ) ) ;
#1447=EDGE_CURVE ( 'NONE', #3727, #10063, #9589, .T. ) ;
#1460=EDGE_CURVE ( 'NONE', #4949, #8739, #2259, .T. ) ;
#1467=EDGE_LOOP ( 'NONE', ( #9505, #5732, #9792, #6843, #4204, #8776 ) ) ;
#1473=CARTESIAN_POINT ( 'NONE',  ( 0.3126073911696294338, 2.020725942163657862, -3.499999999999999556 ) ) ;
#1476=DIRECTION ( 'NONE',  ( 1.000000000000000000, 0.000000000000000000, 0.000000000000000000 ) ) ;
#1478=EDGE_LOOP ( 'NONE', ( #5965, #8680, #5001 ) ) ;
#1516=FACE_OUTER_BOUND ( 'NONE', #7546, .T. ) ;
#1519=CARTESIAN_POINT ( 'NONE',  ( 3.199999999999992628, -3.375361811986524074, -1.153701847711610551 ) ) ;
#1521=VERTEX_POINT ( 'NONE', #7416 ) ;
#1522=CONICAL_SURFACE ( 'NONE', #2060, 4.624785217660733139, 1.047197551196604071 ) ;
#1524=B_SPLINE_CURVE_WITH_KNOTS ( 'NONE', 3,
 ( #7671, #105, #9772, #10661, #3667, #10449 ),
 .UNSPECIFIED., .F., .F.,
 ( 4, 2, 4 ),
 ( 0.002044882221487540584, 0.003063384235218501086, 0.004081886248949461587 ),
 .UNSPECIFIED. ) ;
#1531=DIRECTION ( 'NONE',  ( -1.000000000000000000, -0.000000000000000000, -0.000000000000000000 ) ) ;
#1556=CARTESIAN_POINT ( 'NONE',  ( 3.199999999999999734, -3.031088913245509886, 1.750000000000043077 ) ) ;
#1566=VERTEX_POINT ( 'NONE', #3922 ) ;
#1572=ADVANCED_FACE ( 'NONE', ( #10699 ), #2827, .T. ) ;
#1576=CARTESIAN_POINT ( 'NONE',  ( 2.981723757189247426, 1.693953258775870996, 3.499999999999999112 ) ) ;
#1577=EDGE_LOOP ( 'NONE', ( #10938, #8661, #3163 ) ) ;
#1578=ORIENTED_EDGE ( 'NONE', *, *, #9906, .T. ) ;
#1586=EDGE_CURVE ( 'NONE', #10425, #8904, #3201, .T. ) ;
#1611=CARTESIAN_POINT ( 'NONE',  ( 3.200000000000006839, -3.202582148906703896, 1.452965002680465245 ) ) ;
#1617=VERTEX_POINT ( 'NONE', #9246 ) ;
#1637=CARTESIAN_POINT ( 'NONE',  ( 0.3126073911696503060, 4.041451884327400101, -2.290628625700182053E-14 ) ) ;
#1639=VECTOR ( 'NONE', #6375, 1000.000000000000000 ) ;
#1641=DIRECTION ( 'NONE',  ( 0.000000000000000000, 0.000000000000000000, 1.000000000000000000 ) ) ;
#1645=ORIENTED_EDGE ( 'NONE', *, *, #1262, .F. ) ;
#1658=ADVANCED_FACE ( 'NONE', ( #8477 ), #2108, .T. ) ;
#1678=DIRECTION ( 'NONE',  ( 0.000000000000000000, 0.000000000000000000, 1.000000000000000000 ) ) ;
#1704=AXIS2_PLACEMENT_3D ( 'NONE', #8983, #9925, #2106 ) ;
#1742=AXIS2_PLACEMENT_3D ( 'NONE', #10521, #1970, #10468 ) ;
#1747=DIRECTION ( 'NONE',  ( 1.000000000000000000, 0.000000000000000000, 0.000000000000000000 ) ) ;
#1751=ADVANCED_FACE ( 'NONE', ( #10091 ), #2481, .T. ) ;
#1752=EDGE_LOOP ( 'NONE', ( #3263, #10095, #7264 ) ) ;
#1755=CONICAL_SURFACE ( 'NONE', #9374, 4.624785217660733139, 1.047197551196604071 ) ;
#1776=CARTESIAN_POINT ( 'NONE',  ( 0.000000000000000000, 0.000000000000000000, -3.499999999999999556 ) ) ;
#1777=MANIFOLD_SOLID_BREP ( 'DomeFillet', #10014 ) ;
#1844=EDGE_LOOP ( 'NONE', ( #5665, #3253, #8856, #1996 ) ) ;
#1848=DIRECTION ( 'NONE',  ( 0.000000000000000000, 0.000000000000000000, 1.000000000000000000 ) ) ;
#1864=AXIS2_PLACEMENT_3D ( 'NONE', #4452, #5383, #3772 ) ;
#1881=VECTOR ( 'NONE', #6571, 1000.000000000000114 ) ;
#1891=ORIENTED_EDGE ( 'NONE', *, *, #5988, .F. ) ;
#1894=B_SPLINE_CURVE_WITH_KNOTS ( 'NONE', 3,
 ( #1164, #7114, #432, #1227, #3835, #2008 ),
 .UNSPECIFIED., .F., .F.,
 ( 4, 2, 4 ),
 ( 0.003657268138676071038, 0.004679653797516804964, 0.005702039456357537589 ),
 .UNSPECIFIED. ) ;
#1917=ORIENTED_EDGE ( 'NONE', *, *, #7627, .F. ) ;
#1946=ORIENTED_EDGE ( 'NONE', *, *, #6985, .T. ) ;
#1959=VERTEX_POINT ( 'NONE', #7243 ) ;
#1970=DIRECTION ( 'NONE',  ( -1.000000000000000000, -0.000000000000000000, -0.000000000000000000 ) ) ;
#1987=CARTESIAN_POINT ( 'NONE',  ( 0.02993401039713504061, 2.688325911136429713, -2.343682934607792312 ) ) ;
#1990=CARTESIAN_POINT ( 'NONE',  ( 0.000000000000000000, 2.020667218593133248E-16, -1.650000000000000355 ) ) ;
#1996=ORIENTED_EDGE ( 'NONE', *, *, #6985, .F. ) ;
#2008=CARTESIAN_POINT ( 'NONE',  ( 0.000000000000000000, 0.000000000000000000, 3.499999999999999556 ) ) ;
#2011=ORIENTED_EDGE ( 'NONE', *, *, #1380, .F. ) ;
#2052=DIRECTION ( 'NONE',  ( 1.000000000000000000, 0.000000000000000000, 0.000000000000000000 ) ) ;
#2055=CIRCLE ( 'NONE', #7923, 3.369999999999997886 ) ;
#2058=ORIENTED_EDGE ( 'NONE', *, *, #10990, .F. ) ;
#2060=AXIS2_PLACEMENT_3D ( 'NONE', #4354, #9346, #1678 ) ;
#2066=ORIENTED_EDGE ( 'NONE', *, *, #3077, .F. ) ;
#2068=EDGE_CURVE ( 'NONE', #947, #10875, #5453, .T. ) ;
#2074=FACE_OUTER_BOUND ( 'NONE', #8763, .T. ) ;
#2086=CARTESIAN_POINT ( 'NONE',  ( 3.061158938895378157, 2.351840044243081795, 2.926493552096017137 ) ) ;
#2092=DIRECTION ( 'NONE',  ( -1.000000000000000000, -0.000000000000000000, -0.000000000000000000 ) ) ;
#2106=DIRECTION ( 'NONE',  ( 0.000000000000000000, 0.000000000000000000, 1.000000000000000000 ) ) ;
#2108=CONICAL_SURFACE ( 'NONE', #1031, 4.624785217660733139, 1.047197551196604071 ) ;
#2127=EDGE_CURVE ( 'NONE', #8043, #3326, #7249, .T. ) ;
#2143=DIRECTION ( 'NONE',  ( 0.000000000000000000, 0.000000000000000000, 1.000000000000000000 ) ) ;
#2165=ORIENTED_EDGE ( 'NONE', *, *, #2068, .T. ) ;
#2174=CIRCLE ( 'NONE', #9259, 2.000000000000000000 ) ;
#2190=UNCERTAINTY_MEASURE_WITH_UNIT (LENGTH_MEASURE( 1.000000000000000082E-05 ), #401, 'distance_accuracy_value', 'NONE');
#2198=CARTESIAN_POINT ( 'NONE',  ( 0.000000000000000000, -3.031088913245550298, -1.749999999999972911 ) ) ;
#2217=ORIENTED_EDGE ( 'NONE', *, *, #158, .F. ) ;
#2241=AXIS2_PLACEMENT_3D ( 'NONE', #7633, #6509, #2300 ) ;
#2247=DIRECTION ( 'NONE',  ( -1.000000000000000000, -0.000000000000000000, -0.000000000000000000 ) ) ;
#2259=LINE ( 'NONE', #3873, #10333 ) ;
#2296=DIRECTION ( 'NONE',  ( -1.000000000000000000, 0.000000000000000000, -0.000000000000000000 ) ) ;
#2300=DIRECTION ( 'NONE',  ( 0.000000000000000000, 0.000000000000000000, -1.000000000000000000 ) ) ;
#2323=ORIENTED_EDGE ( 'NONE', *, *, #3148, .F. ) ;
#2337=CARTESIAN_POINT ( 'NONE',  ( 3.169801662054988700, 0.6882444255503921138, -3.499999999999999556 ) ) ;
#2340=ORIENTED_EDGE ( 'NONE', *, *, #3572, .T. ) ;
#2355=DIRECTION ( 'NONE',  ( 1.000000000000000000, 0.000000000000000000, 0.000000000000000000 ) ) ;
#2365=CARTESIAN_POINT ( 'NONE',  ( 0.000000000000000000, 0.000000000000000000, 0.000000000000000000 ) ) ;
#2366=DIRECTION ( 'NONE',  ( 0.000000000000000000, 0.000000000000000000, 1.000000000000000000 ) ) ;
#2379=ORIENTED_EDGE ( 'NONE', *, *, #4794, .F. ) ;
#2383=FACE_OUTER_BOUND ( 'NONE', #5884, .T. ) ;
#2405=PLANE ( 'NONE',  #8449 ) ;
#2418=ADVANCED_FACE ( 'NONE', ( #5036 ), #1276, .F. ) ;
#2422=CARTESIAN_POINT ( 'NONE',  ( 3.200000000000000178, 0.000000000000000000, 0.000000000000000000 ) ) ;
#2469=CARTESIAN_POINT ( 'NONE',  ( 0.02993401039711700642, -2.688325911136495883, 2.343682934607659529 ) ) ;
#2474=CARTESIAN_POINT ( 'NONE',  ( 0.000000000000000000, 3.031088913245510774, -1.750000000000042411 ) ) ;
#2481=CYLINDRICAL_SURFACE ( 'NONE', #1211, 3.249999999999998224 ) ;
#2512=AXIS2_PLACEMENT_3D ( 'NONE', #9590, #6092, #10439 ) ;
#2513=CARTESIAN_POINT ( 'NONE',  ( 0.2704726383733979667, 0.000000000000000000, 0.000000000000000000 ) ) ;
#2519=DIRECTION ( 'NONE',  ( 0.000000000000000000, 0.000000000000000000, -1.000000000000000000 ) ) ;
#2522=DIRECTION ( 'NONE',  ( 0.000000000000000000, 0.000000000000000000, -1.000000000000000000 ) ) ;
#2536=AXIS2_PLACEMENT_3D ( 'NONE', #10062, #5128, #886 ) ;
#2546=ORIENTED_EDGE ( 'NONE', *, *, #1447, .T. ) ;
#2557=FACE_OUTER_BOUND ( 'NONE', #10081, .T. ) ;
#2580=DIRECTION ( 'NONE',  ( 0.000000000000000000, -0.5000000000000121014, -0.8660254037844316022 ) ) ;
#2649=CARTESIAN_POINT ( 'NONE',  ( 0.000000000000000000, 3.031088913245550742, 1.749999999999972466 ) ) ;
#2658=CARTESIAN_POINT ( 'NONE',  ( 3.078243469714899039, -2.351289329882112256, 2.927447417349546832 ) ) ;
#2659=EDGE_LOOP ( 'NONE', ( #1178, #4674, #7916, #5071 ) ) ;
#2665=FACE_OUTER_BOUND ( 'NONE', #7272, .T. ) ;
#2669=CARTESIAN_POINT ( 'NONE',  ( 0.2182762428107343500, 1.693953258775802606, -3.499999999999999556 ) ) ;
#2700=AXIS2_PLACEMENT_3D ( 'NONE', #2868, #400, #10585 ) ;
#2721=ORIENTED_EDGE ( 'NONE', *, *, #1586, .F. ) ;
#2723=FACE_BOUND ( 'NONE', #3713, .T. ) ;
#2752=ADVANCED_FACE ( 'NONE', ( #8966 ), #8190, .T. ) ;
#2756=DIRECTION ( 'NONE',  ( 1.000000000000000000, -0.000000000000000000, -0.000000000000000000 ) ) ;
#2760=CARTESIAN_POINT ( 'NONE',  ( 8.000000000000000000, -1.423651904008798069E-15, 0.000000000000000000 ) ) ;
#2764=CARTESIAN_POINT ( 'NONE',  ( 4.750000000000000888, 0.000000000000000000, 0.000000000000000000 ) ) ;
#2769=UNCERTAINTY_MEASURE_WITH_UNIT (LENGTH_MEASURE( 1.000000000000000082E-05 ), #10761, 'distance_accuracy_value', 'NONE');
#2776=CARTESIAN_POINT ( 'NONE',  ( 0.1217565302851224412, 2.351289329882196633, 2.927447417349528624 ) ) ;
#2777=DIRECTION ( 'NONE',  ( 0.000000000000000000, 1.224646799147353207E-16, -1.000000000000000000 ) ) ;
#2794=AXIS2_PLACEMENT_3D ( 'NONE', #7301, #3868, #9758 ) ;
#2799=STYLED_ITEM ( 'NONE', ( #876 ), #4816 ) ;
#2811=CARTESIAN_POINT ( 'NONE',  ( 3.319999999999999840, 3.980102097228895766E-16, -3.249999999999998224 ) ) ;
#2827=CONICAL_SURFACE ( 'NONE', #3703, 3.499999999999999556, 1.047197551196603849 ) ;
#2830=EDGE_CURVE ( 'NONE', #4665, #8097, #9676, .T. ) ;
#2831=CARTESIAN_POINT ( 'NONE',  ( 0.000000000000000000, 3.031088913245510774, -1.750000000000042411 ) ) ;
#2835=DIRECTION ( 'NONE',  ( 1.000000000000000000, 0.000000000000000000, 0.000000000000000000 ) ) ;
#2843=DIRECTION ( 'NONE',  ( 0.000000000000000000, 0.000000000000000000, -1.000000000000000000 ) ) ;
#2849=CARTESIAN_POINT ( 'NONE',  ( 0.3126073911696503060, 4.041451884327400101, -2.290628625700182053E-14 ) ) ;
#2863=VERTEX_POINT ( 'NONE', #1412 ) ;
#2867=CARTESIAN_POINT ( 'NONE',  ( 0.3126073911691547025, -2.020725942164465661, -3.499999999999999556 ) ) ;
#2868=CARTESIAN_POINT ( 'NONE',  ( 2.550604951803072673, 0.000000000000000000, 0.000000000000000000 ) ) ;
#2869=LINE ( 'NONE', #9694, #4763 ) ;
#2901=VERTEX_POINT ( 'NONE', #3353 ) ;
#2903=ORIENTED_EDGE ( 'NONE', *, *, #4860, .F. ) ;
#2907=EDGE_CURVE ( 'NONE', #10134, #9486, #9248, .T. ) ;
#2920=DIRECTION ( 'NONE',  ( 0.000000000000000000, 0.000000000000000000, -1.000000000000000000 ) ) ;
#2922=CARTESIAN_POINT ( 'NONE',  ( 3.199999999999999734, 3.031088913245550742, 1.749999999999972466 ) ) ;
#2927=LINE ( 'NONE', #4759, #5429 ) ;
#2934=DIRECTION ( 'NONE',  ( 1.000000000000000000, -0.000000000000000000, -0.000000000000000000 ) ) ;
#2939=CARTESIAN_POINT ( 'NONE',  ( 0.000000000000000000, 3.031088913245550742, 1.749999999999972466 ) ) ;
#2948=VECTOR ( 'NONE', #10844, 1000.000000000000000 ) ;
#2950=AXIS2_PLACEMENT_3D ( 'NONE', #5326, #2835, #9036 ) ;
#2977=CARTESIAN_POINT ( 'NONE',  ( 0.000000000000000000, 0.000000000000000000, 0.000000000000000000 ) ) ;
#2978=CARTESIAN_POINT ( 'NONE',  ( 0.3126073911691547025, -2.020725942164465661, -3.499999999999999556 ) ) ;
#3009=ORIENTED_EDGE ( 'NONE', *, *, #3762, .F. ) ;
#3028=CARTESIAN_POINT ( 'NONE',  ( 4.750000000000000888, -1.622657008870242882E-15, 0.000000000000000000 ) ) ;
#3059=DIRECTION ( 'NONE',  ( 0.000000000000000000, 0.000000000000000000, 1.000000000000000000 ) ) ;
#3074=PLANE ( 'NONE',  #4366 ) ;
#3077=EDGE_CURVE ( 'NONE', #6815, #58, #6410, .T. ) ;
#3105=VERTEX_POINT ( 'NONE', #3602 ) ;
#3113=ORIENTED_EDGE ( 'NONE', *, *, #6691, .F. ) ;
#3114=VECTOR ( 'NONE', #8464, 1000.000000000000114 ) ;
#3116=CARTESIAN_POINT ( 'NONE',  ( 0.2176891316980170965, -1.691919446222082346, -3.499999999999999112 ) ) ;
#3125=AXIS2_PLACEMENT_3D ( 'NONE', #9351, #1747, #3410 ) ;
#3141=CARTESIAN_POINT ( 'NONE',  ( 2.887392608830372964, -2.020725942163647648, 3.499999999999999556 ) ) ;
#3148=EDGE_CURVE ( 'NONE', #8043, #9486, #8725, .T. ) ;
#3149=ADVANCED_FACE ( 'NONE', ( #9544 ), #9507, .T. ) ;
#3150=LINE ( 'NONE', #532, #8420 ) ;
#3156=CARTESIAN_POINT ( 'NONE',  ( 3.061158938895440773, -2.351840044243218131, -2.926493552095763118 ) ) ;
#3159=DIRECTION ( 'NONE',  ( 0.000000000000000000, 0.000000000000000000, 1.000000000000000000 ) ) ;
#3161=EDGE_CURVE ( 'NONE', #7127, #6258, #8042, .T. ) ;
#3163=ORIENTED_EDGE ( 'NONE', *, *, #7859, .T. ) ;
#3164=STYLED_ITEM ( 'NONE', ( #8028 ), #1777 ) ;
#3168=EDGE_CURVE ( 'NONE', #9486, #7127, #4898, .T. ) ;
#3193=CARTESIAN_POINT ( 'NONE',  ( 3.170625919164821394, -0.6808742863894992059, 3.500000000000000000 ) ) ;
#3201=B_SPLINE_CURVE_WITH_KNOTS ( 'NONE', 3,
 ( #5702, #1426, #3193, #9975, #8094, #3141 ),
 .UNSPECIFIED., .F., .F.,
 ( 4, 2, 4 ),
 ( 0.01103649464086231546, 0.01205977283736816077, 0.01308305103387400609 ),
 .UNSPECIFIED. ) ;
#3213=( NAMED_UNIT ( * ) PLANE_ANGLE_UNIT ( ) SI_UNIT ( $, .RADIAN. ) );
#3223=DIRECTION ( 'NONE',  ( 0.000000000000000000, -0.8660254037844431485, -0.4999999999999921729 ) ) ;
#3225=PRODUCT_DEFINITION_CONTEXT ( 'detailed design', #8765, 'design' ) ;
#3253=ORIENTED_EDGE ( 'NONE', *, *, #10957, .T. ) ;
#3263=ORIENTED_EDGE ( 'NONE', *, *, #2830, .T. ) ;
#3287=CONICAL_SURFACE ( 'NONE', #611, 3.499999999999999556, 1.047197551196603849 ) ;
#3300=CARTESIAN_POINT ( 'NONE',  ( 3.200000000000000178, 0.3418418480469889165, 3.499999999999999556 ) ) ;
#3302=ORIENTED_EDGE ( 'NONE', *, *, #3148, .T. ) ;
#3313=CIRCLE ( 'NONE', #438, 1.650000000000000355 ) ;
#3326=VERTEX_POINT ( 'NONE', #26 ) ;
#3328=FILL_AREA_STYLE_COLOUR ( '', #476 ) ;
#3329=VERTEX_POINT ( 'NONE', #9303 ) ;
#3339=CIRCLE ( 'NONE', #851, 3.249999999999998668 ) ;
#3348=EDGE_CURVE ( 'NONE', #58, #6815, #2055, .T. ) ;
#3353=CARTESIAN_POINT ( 'NONE',  ( 5.791420021395468964, -3.168237633705329831E-17, 0.000000000000000000 ) ) ;
#3369=CARTESIAN_POINT ( 'NONE',  ( 0.000000000000000000, 3.031088913245510774, -1.750000000000042411 ) ) ;
#3410=DIRECTION ( 'NONE',  ( 0.000000000000000000, 0.000000000000000000, -1.000000000000000000 ) ) ;
#3411=CARTESIAN_POINT ( 'NONE',  ( 0.000000000000000000, -3.031088913245509886, 1.750000000000043077 ) ) ;
#3414=VERTEX_POINT ( 'NONE', #4139 ) ;
#3415=CARTESIAN_POINT ( 'NONE',  ( 0.1388410611046201060, 3.710337782248057437, 0.5735064479039569951 ) ) ;
#3420=PRODUCT_DEFINITION ( 'UNKNOWN', '', #7574, #3225 ) ;
#3428=DIRECTION ( 'NONE',  ( -1.000000000000000000, -0.000000000000000000, -0.000000000000000000 ) ) ;
#3443=CONICAL_SURFACE ( 'NONE', #5025, 3.499999999999999556, 1.047197551196603849 ) ;
#3444=CARTESIAN_POINT ( 'NONE',  ( 3.199999999999999734, 0.000000000000000000, -3.499999999999999556 ) ) ;
#3446=EDGE_LOOP ( 'NONE', ( #9862, #2058, #1946, #9965 ) ) ;
#3464=AXIS2_PLACEMENT_3D ( 'NONE', #7721, #41, #8493 ) ;
#3468=AXIS2_PLACEMENT_3D ( 'NONE', #6756, #5105, #10154 ) ;
#3506=LINE ( 'NONE', #4110, #834 ) ;
#3512=ORIENTED_EDGE ( 'NONE', *, *, #4393, .T. ) ;
#3525=( GEOMETRIC_REPRESENTATION_CONTEXT ( 3 ) GLOBAL_UNCERTAINTY_ASSIGNED_CONTEXT ( ( #2190 ) ) GLOBAL_UNIT_ASSIGNED_CONTEXT ( ( #401, #8748, #4594 ) ) REPRESENTATION_CONTEXT ( 'NONE', 'WORKASPACE' ) );
#3551=EDGE_LOOP ( 'NONE', ( #6107, #6565, #9396 ) ) ;
#3557=ORIENTED_EDGE ( 'NONE', *, *, #10421, .F. ) ;
#3558=CARTESIAN_POINT ( 'NONE',  ( 2.887392608830349428, 4.041451884327400101, -2.289061810243902218E-14 ) ) ;
#3565=DIRECTION ( 'NONE',  ( 0.000000000000000000, 0.000000000000000000, -1.000000000000000000 ) ) ;
#3572=EDGE_CURVE ( 'NONE', #8904, #7419, #10754, .T. ) ;
#3578=DIRECTION ( 'NONE',  ( 0.000000000000000000, 1.000000000000000000, 0.000000000000000000 ) ) ;
#3586=DIRECTION ( 'NONE',  ( 0.000000000000000000, 0.000000000000000000, -1.000000000000000000 ) ) ;
#3587=DIRECTION ( 'NONE',  ( 0.000000000000000000, -1.000000000000000000, 0.000000000000000000 ) ) ;
#3602=CARTESIAN_POINT ( 'NONE',  ( 0.02539999999999975264, 2.449293598294706414E-16, 2.000000000000000000 ) ) ;
#3636=DIRECTION ( 'NONE',  ( 0.000000000000000000, 0.000000000000000000, -1.000000000000000000 ) ) ;
#3637=AXIS2_PLACEMENT_3D ( 'NONE', #10539, #2934, #10433 ) ;
#3641=DIRECTION ( 'NONE',  ( 1.000000000000000000, -0.000000000000000000, -0.000000000000000000 ) ) ;
#3655=CARTESIAN_POINT ( 'NONE',  ( 3.078243469714894598, 2.351289329882122914, -2.927447417349547720 ) ) ;
#3667=CARTESIAN_POINT ( 'NONE',  ( 0.2174200650117590894, -3.876582599186223721, -0.2855619784720447862 ) ) ;
#3683=AXIS2_PLACEMENT_3D ( 'NONE', #708, #10942, #5943 ) ;
#3692=CARTESIAN_POINT ( 'NONE',  ( 0.1217565302850657921, -2.351289329882329859, -2.927447417349280823 ) ) ;
#3703=AXIS2_PLACEMENT_3D ( 'NONE', #9870, #1476, #9035 ) ;
#3713=EDGE_LOOP ( 'NONE', ( #9917, #6712 ) ) ;
#3716=ADVANCED_FACE ( 'NONE', ( #4645 ), #617, .T. ) ;
#3717=PLANE ( 'NONE',  #1864 ) ;
#3727=VERTEX_POINT ( 'NONE', #403 ) ;
#3732=EDGE_CURVE ( 'NONE', #1959, #10050, #2927, .T. ) ;
#3753=ORIENTED_EDGE ( 'NONE', *, *, #1380, .T. ) ;
#3762=EDGE_CURVE ( 'NONE', #7127, #3326, #4904, .T. ) ;
#3772=DIRECTION ( 'NONE',  ( 0.000000000000000000, -0.4999999999999922839, 0.8660254037844430375 ) ) ;
#3806=CARTESIAN_POINT ( 'NONE',  ( 0.000000000000000000, -3.031088913245509886, 1.750000000000043077 ) ) ;
#3809=CIRCLE ( 'NONE', #778, 3.499999999999999556 ) ;
#3835=CARTESIAN_POINT ( 'NONE',  ( 2.371692252312040949E-17, -0.3416191432522661664, 3.499999999999999112 ) ) ;
#3856=CARTESIAN_POINT ( 'NONE',  ( 0.03019833794501310467, 0.6882444255504208686, 3.500000000000000444 ) ) ;
#3865=AXIS2_PLACEMENT_3D ( 'NONE', #8053, #9666, #8777 ) ;
#3868=DIRECTION ( 'NONE',  ( 1.000000000000000000, 0.000000000000000000, 0.000000000000000000 ) ) ;
#3873=CARTESIAN_POINT ( 'NONE',  ( 0.000000000000000000, 0.000000000000000000, 1.650000000000000355 ) ) ;
#3877=CARTESIAN_POINT ( 'NONE',  ( 0.000000000000000000, 0.000000000000000000, 0.000000000000000000 ) ) ;
#3888=FACE_OUTER_BOUND ( 'NONE', #3934, .T. ) ;
#3895=ADVANCED_FACE ( 'NONE', ( #10964 ), #9289, .F. ) ;
#3896=CARTESIAN_POINT ( 'NONE',  ( 0.000000000000000000, 0.000000000000000000, -3.499999999999999556 ) ) ;
#3897=EDGE_CURVE ( 'NONE', #4107, #8160, #5969, .T. ) ;
#3910=ADVANCED_FACE ( 'NONE', ( #1516 ), #2405, .F. ) ;
#3922=CARTESIAN_POINT ( 'NONE',  ( 3.199999999999999734, 0.000000000000000000, -3.499999999999999556 ) ) ;
#3928=ADVANCED_FACE ( 'NONE', ( #6790, #5962 ), #899, .F. ) ;
#3934=EDGE_LOOP ( 'NONE', ( #5829, #3512, #332, #4799 ) ) ;
#3935=CARTESIAN_POINT ( 'NONE',  ( 3.170065989602867784, -2.688325911136562052, -2.343682934607623558 ) ) ;
#3990=VERTEX_POINT ( 'NONE', #2198 ) ;
#3999=VECTOR ( 'NONE', #4815, 1000.000000000000000 ) ;
#4001=CIRCLE ( 'NONE', #5090, 3.499999999999997780 ) ;
#4021=DIRECTION ( 'NONE',  ( 0.000000000000000000, 0.000000000000000000, -1.000000000000000000 ) ) ;
#4036=B_SPLINE_CURVE_WITH_KNOTS ( 'NONE', 3,
 ( #5587, #10592, #8972, #3806 ),
 .UNSPECIFIED., .F., .F.,
 ( 4, 4 ),
 ( 2.380739282168429972E-07, 0.002044882221487562268 ),
 .UNSPECIFIED. ) ;
#4055=SHAPE_REPRESENTATION_RELATIONSHIP ( 'NONE' , 'NONE' ,  #7975, #4816 ) ;
#4064=FACE_OUTER_BOUND ( 'NONE', #10247, .T. ) ;
#4071=LINE ( 'NONE', #4803, #2948 ) ;
#4097=ORIENTED_EDGE ( 'NONE', *, *, #3168, .F. ) ;
#4107=VERTEX_POINT ( 'NONE', #10854 ) ;
#4110=CARTESIAN_POINT ( 'NONE',  ( 0.2949799022107380542, 0.000000000000000000, 1.615000000000000213 ) ) ;
#4114=CARTESIAN_POINT ( 'NONE',  ( 0.000000000000000000, 0.000000000000000000, 0.000000000000000000 ) ) ;
#4121=CARTESIAN_POINT ( 'NONE',  ( 3.199999999999999734, 0.000000000000000000, 3.499999999999999556 ) ) ;
#4131=CARTESIAN_POINT ( 'NONE',  ( 1.192664741381417277E-14, 3.202582148906763848, 1.452965002680410178 ) ) ;
#4139=CARTESIAN_POINT ( 'NONE',  ( 2.887392608830349428, 4.041451884327400101, -2.289061810243902218E-14 ) ) ;
#4142=CARTESIAN_POINT ( 'NONE',  ( 4.800000000000000711, 0.000000000000000000, 1.649999999999999911 ) ) ;
#4144=AXIS2_PLACEMENT_3D ( 'NONE', #7104, #205, #7885 ) ;
#4155=CARTESIAN_POINT ( 'NONE',  ( 2.887392608830845031, -2.020725942164465661, -3.499999999999999556 ) ) ;
#4163=EDGE_CURVE ( 'NONE', #702, #1566, #4001, .T. ) ;
#4169=CONICAL_SURFACE ( 'NONE', #1155, 3.499999999999999556, 1.047197551196603849 ) ;
#4181=AXIS2_PLACEMENT_3D ( 'NONE', #6239, #2756, #10527 ) ;
#4185=CARTESIAN_POINT ( 'NONE',  ( 4.750000000000000888, 0.000000000000000000, 0.000000000000000000 ) ) ;
#4189=CARTESIAN_POINT ( 'NONE',  ( 3.199999999999999734, -3.031088913245550298, -1.749999999999972911 ) ) ;
#4192=ORIENTED_EDGE ( 'NONE', *, *, #4794, .T. ) ;
#4200=EDGE_CURVE ( 'NONE', #10068, #783, #5200, .T. ) ;
#4204=ORIENTED_EDGE ( 'NONE', *, *, #10641, .T. ) ;
#4248=DIRECTION ( 'NONE',  ( 0.000000000000000000, 0.000000000000000000, -1.000000000000000000 ) ) ;
#4253=ORIENTED_EDGE ( 'NONE', *, *, #5298, .F. ) ;
#4278=FILL_AREA_STYLE ('',( #3328 ) ) ;
#4296=DIRECTION ( 'NONE',  ( 0.000000000000000000, 0.000000000000000000, 1.000000000000000000 ) ) ;
#4304=B_SPLINE_CURVE_WITH_KNOTS ( 'NONE', 3,
 ( #9164, #9107, #714, #2337, #9058, #665 ),
 .UNSPECIFIED., .F., .F.,
 ( 4, 2, 4 ),
 ( 0.008988604078116352661, 0.01001254935948927942, 0.01103649464086220618 ),
 .UNSPECIFIED. ) ;
#4330=CARTESIAN_POINT ( 'NONE',  ( 0.1397399040437465878, 1.362955318038519659, -3.499999999999999556 ) ) ;
#4332=CARTESIAN_POINT ( 'NONE',  ( 3.061857526609890190, -1.355358988605575021, -3.499999999999999556 ) ) ;
#4348=VERTEX_POINT ( 'NONE', #2811 ) ;
#4354=CARTESIAN_POINT ( 'NONE',  ( 2.550604951803072673, 0.000000000000000000, 0.000000000000000000 ) ) ;
#4361=CARTESIAN_POINT ( 'NONE',  ( -6.921953244962140004E-15, -2.859595677584344298, 2.047034997319538085 ) ) ;
#4366=AXIS2_PLACEMENT_3D ( 'NONE', #6447, #7340, #2296 ) ;
#4377=VERTEX_POINT ( 'NONE', #6967 ) ;
#4387=AXIS2_PLACEMENT_3D ( 'NONE', #8799, #7083, #3586 ) ;
#4393=EDGE_CURVE ( 'NONE', #10063, #4377, #5308, .T. ) ;
#4404=DIRECTION ( 'NONE',  ( 0.000000000000000000, 0.000000000000000000, -1.000000000000000000 ) ) ;
#4418=CIRCLE ( 'NONE', #5485, 3.499999999999999556 ) ;
#4452=CARTESIAN_POINT ( 'NONE',  ( 3.200000000000000178, -4.041451884327390331, 2.328587628042611615E-14 ) ) ;
#4483=CARTESIAN_POINT ( 'NONE',  ( 4.750000000000000888, 3.980102097228896752E-16, -3.249999999999999112 ) ) ;
#4488=CARTESIAN_POINT ( 'NONE',  ( 3.200000000000006395, -2.686816014504533001, 2.346298152288395666 ) ) ;
#4503=ORIENTED_EDGE ( 'NONE', *, *, #131, .T. ) ;
#4528=DIRECTION ( 'NONE',  ( 0.000000000000000000, 0.000000000000000000, 1.000000000000000000 ) ) ;
#4536=EDGE_CURVE ( 'NONE', #7419, #702, #790, .T. ) ;
#4571=ADVANCED_FACE ( 'NONE', ( #6370 ), #8427, .F. ) ;
#4590=DIRECTION ( 'NONE',  ( -0.000000000000000000, 0.000000000000000000, 1.000000000000000000 ) ) ;
#4594=( NAMED_UNIT ( * ) SI_UNIT ( $, .STERADIAN. ) SOLID_ANGLE_UNIT ( ) );
#4645=FACE_OUTER_BOUND ( 'NONE', #1478, .T. ) ;
#4662=CONICAL_SURFACE ( 'NONE', #36, 1.615000000000000213, 0.9599310885968811435 ) ;
#4665=VERTEX_POINT ( 'NONE', #5857 ) ;
#4667=EDGE_CURVE ( 'NONE', #783, #8160, #10283, .T. ) ;
#4674=ORIENTED_EDGE ( 'NONE', *, *, #623, .T. ) ;
#4686=DIRECTION ( 'NONE',  ( -1.000000000000000000, -0.000000000000000000, -0.000000000000000000 ) ) ;
#4695=CARTESIAN_POINT ( 'NONE',  ( 0.000000000000000000, 3.031088913245550742, 1.749999999999972466 ) ) ;
#4713=CARTESIAN_POINT ( 'NONE',  ( 3.200000000000000178, -2.020725942163647648, 3.499999999999999556 ) ) ;
#4719=AXIS2_PLACEMENT_3D ( 'NONE', #7409, #2355, #4021 ) ;
#4750=ORIENTED_EDGE ( 'NONE', *, *, #10041, .F. ) ;
#4759=CARTESIAN_POINT ( 'NONE',  ( 3.200000000000000178, -2.020725942163728028, -3.499999999999999556 ) ) ;
#4763=VECTOR ( 'NONE', #3641, 1000.000000000000000 ) ;
#4778=CARTESIAN_POINT ( 'NONE',  ( 0.3126073911691312213, -2.020725942164384836, 3.499999999999999556 ) ) ;
#4794=EDGE_CURVE ( 'NONE', #3414, #4665, #9356, .T. ) ;
#4799=ORIENTED_EDGE ( 'NONE', *, *, #10746, .F. ) ;
#4803=CARTESIAN_POINT ( 'NONE',  ( 3.200000000000000178, 4.041451884327400101, -2.303506639521620593E-14 ) ) ;
#4809=EDGE_LOOP ( 'NONE', ( #9316, #9508, #850, #3113, #278, #2721 ) ) ;
#4815=DIRECTION ( 'NONE',  ( -1.000000000000000000, -0.000000000000000000, -0.000000000000000000 ) ) ;
#4816=ADVANCED_BREP_SHAPE_REPRESENTATION ( '', ( #1777, #308 ), #8995 ) ;
#4841=EDGE_CURVE ( 'NONE', #10063, #8739, #3313, .T. ) ;
#4859=CARTESIAN_POINT ( 'NONE',  ( 4.800000000000000711, 0.000000000000000000, 0.000000000000000000 ) ) ;
#4860=EDGE_CURVE ( 'NONE', #947, #6804, #6122, .T. ) ;
#4878=DIRECTION ( 'NONE',  ( -1.000000000000000000, -0.000000000000000000, -0.000000000000000000 ) ) ;
#4890=CARTESIAN_POINT ( 'NONE',  ( 3.200000000000000178, 4.127059713126577826E-16, 3.369999999999997886 ) ) ;
#4892=CARTESIAN_POINT ( 'NONE',  ( 3.199999999999999734, 0.000000000000000000, 0.000000000000000000 ) ) ;
#4898=CIRCLE ( 'NONE', #1704, 3.249999999999998668 ) ;
#4904=CIRCLE ( 'NONE', #9337, 3.249999999999998668 ) ;
#4923=CARTESIAN_POINT ( 'NONE',  ( 0.3126073911696503060, 4.041451884327400101, -2.290628625700182053E-14 ) ) ;
#4930=EDGE_CURVE ( 'NONE', #3329, #6272, #1341, .T. ) ;
#4936=CIRCLE ( 'NONE', #7766, 3.499999999999997780 ) ;
#4947=ORIENTED_EDGE ( 'NONE', *, *, #4841, .F. ) ;
#4948=DIRECTION ( 'NONE',  ( -1.000000000000000000, -0.000000000000000000, -0.000000000000000000 ) ) ;
#4949=VERTEX_POINT ( 'NONE', #4142 ) ;
#4974=ORIENTED_EDGE ( 'NONE', *, *, #3897, .T. ) ;
#4975=CARTESIAN_POINT ( 'NONE',  ( 3.060260095956242488, 1.362955318038574948, 3.500000000000000000 ) ) ;
#4993=AXIS2_PLACEMENT_3D ( 'NONE', #9133, #8247, #1641 ) ;
#5001=ORIENTED_EDGE ( 'NONE', *, *, #4536, .F. ) ;
#5008=CARTESIAN_POINT ( 'NONE',  ( 3.061158938895391923, -3.710337782248029015, 0.5735064479040067331 ) ) ;
#5016=PRODUCT ( 'domed cap nut_din_DIN 1587 - M4 --NNU', 'domed cap nut_din_DIN 1587 - M4 --NNU', '', ( #8715 ) ) ;
#5025=AXIS2_PLACEMENT_3D ( 'NONE', #4114, #10118, #8389 ) ;
#5036=FACE_OUTER_BOUND ( 'NONE', #5547, .T. ) ;
#5050=ORIENTED_EDGE ( 'NONE', *, *, #9052, .T. ) ;
#5071=ORIENTED_EDGE ( 'NONE', *, *, #9052, .F. ) ;
#5077=ORIENTED_EDGE ( 'NONE', *, *, #5988, .T. ) ;
#5085=LINE ( 'NONE', #7807, #3114 ) ;
#5086=CARTESIAN_POINT ( 'NONE',  ( 3.319999999999999840, 0.000000000000000000, 0.000000000000000000 ) ) ;
#5090=AXIS2_PLACEMENT_3D ( 'NONE', #9125, #10022, #2522 ) ;
#5096=DIRECTION ( 'NONE',  ( -1.000000000000000000, -0.000000000000000000, -0.000000000000000000 ) ) ;
#5099=B_SPLINE_CURVE_WITH_KNOTS ( 'NONE', 3,
 ( #1556, #1611, #10171, #5008, #8330, #9160 ),
 .UNSPECIFIED., .F., .F.,
 ( 4, 2, 4 ),
 ( 0.002044882221487497216, 0.003063384235218479402, 0.004081886248949461587 ),
 .UNSPECIFIED. ) ;
#5105=DIRECTION ( 'NONE',  ( -1.000000000000000000, -0.000000000000000000, -0.000000000000000000 ) ) ;
#5116=SURFACE_STYLE_FILL_AREA ( #4278 ) ;
#5128=DIRECTION ( 'NONE',  ( 0.000000000000000000, 1.000000000000000000, -1.224646799147353207E-16 ) ) ;
#5138=FACE_OUTER_BOUND ( 'NONE', #1752, .T. ) ;
#5145=ORIENTED_EDGE ( 'NONE', *, *, #3572, .F. ) ;
#5167=CARTESIAN_POINT ( 'NONE',  ( 0.03019833794501056504, 0.6882444255503935571, -3.500000000000000000 ) ) ;
#5191=CARTESIAN_POINT ( 'NONE',  ( 0.3126073911691312213, -2.020725942164384836, 3.499999999999999556 ) ) ;
#5198=B_SPLINE_CURVE_WITH_KNOTS ( 'NONE', 3,
 ( #1776, #9380, #5167, #4330, #2669, #6044 ),
 .UNSPECIFIED., .F., .F.,
 ( 4, 2, 4 ),
 ( 0.005702039456357650346, 0.006725091618211351784, 0.007748143780065053221 ),
 .UNSPECIFIED. ) ;
#5200=B_SPLINE_CURVE_WITH_KNOTS ( 'NONE', 3,
 ( #2649, #4131, #5797, #3415, #9186, #4923 ),
 .UNSPECIFIED., .F., .F.,
 ( 4, 2, 4 ),
 ( 0.002044882221487536681, 0.003063384235218498050, 0.004081886248949459853 ),
 .UNSPECIFIED. ) ;
#5202=DIRECTION ( 'NONE',  ( 1.000000000000000000, 0.000000000000000000, 0.000000000000000000 ) ) ;
#5242=CARTESIAN_POINT ( 'NONE',  ( 0.2949799022107380542, 0.000000000000000000, 0.000000000000000000 ) ) ;
#5288=ORIENTED_EDGE ( 'NONE', *, *, #10319, .T. ) ;
#5298=EDGE_CURVE ( 'NONE', #947, #10068, #4418, .T. ) ;
#5308=LINE ( 'NONE', #344, #10230 ) ;
#5326=CARTESIAN_POINT ( 'NONE',  ( 0.000000000000000000, 0.000000000000000000, 0.000000000000000000 ) ) ;
#5337=FACE_OUTER_BOUND ( 'NONE', #1844, .T. ) ;
#5348=ADVANCED_FACE ( 'NONE', ( #2074 ), #1755, .T. ) ;
#5359=AXIS2_PLACEMENT_3D ( 'NONE', #6988, #2777, #6150 ) ;
#5361=CARTESIAN_POINT ( 'NONE',  ( 6.673314278414740999E-15, -2.686816014504674222, -2.346298152288229577 ) ) ;
#5365=SURFACE_STYLE_USAGE ( .BOTH. , #10256 ) ;
#5374=CARTESIAN_POINT ( 'NONE',  ( 0.1388410611046027587, 2.351840044243008965, -2.926493552096035788 ) ) ;
#5383=DIRECTION ( 'NONE',  ( -0.000000000000000000, 0.8660254037844431485, 0.4999999999999923395 ) ) ;
#5393=ORIENTED_EDGE ( 'NONE', *, *, #9877, .F. ) ;
#5413=CARTESIAN_POINT ( 'NONE',  ( 3.199999999999999734, 3.031088913245550742, 1.749999999999972466 ) ) ;
#5416=DIRECTION ( 'NONE',  ( 1.000000000000000000, 0.000000000000000000, 0.000000000000000000 ) ) ;
#5417=DIRECTION ( 'NONE',  ( 1.000000000000000000, 0.000000000000000000, 0.000000000000000000 ) ) ;
#5419=DIRECTION ( 'NONE',  ( 0.000000000000000000, 0.000000000000000000, -1.000000000000000000 ) ) ;
#5429=VECTOR ( 'NONE', #2247, 1000.000000000000000 ) ;
#5453=B_SPLINE_CURVE_WITH_KNOTS ( 'NONE', 3,
 ( #7289, #8964, #3856, #1187, #7241, #10731 ),
 .UNSPECIFIED., .F., .F.,
 ( 4, 2, 4 ),
 ( 0.005702039456357537589, 0.006725091618211279793, 0.007748143780065021996 ),
 .UNSPECIFIED. ) ;
#5485=AXIS2_PLACEMENT_3D ( 'NONE', #7174, #4686, #8688 ) ;
#5502=EDGE_CURVE ( 'NONE', #702, #1959, #9210, .T. ) ;
#5518=CARTESIAN_POINT ( 'NONE',  ( 2.550604951803072673, 0.000000000000000000, 0.000000000000000000 ) ) ;
#5547=EDGE_LOOP ( 'NONE', ( #2217, #8490, #10967 ) ) ;
#5551=EDGE_CURVE ( 'NONE', #3326, #10134, #3339, .T. ) ;
#5552=ORIENTED_EDGE ( 'NONE', *, *, #5551, .F. ) ;
#5574=CARTESIAN_POINT ( 'NONE',  ( 2.887392608830370744, 2.020725942163657862, -3.499999999999999556 ) ) ;
#5587=CARTESIAN_POINT ( 'NONE',  ( 0.3126073911696448659, -4.041451884327390331, 2.328673539876467720E-14 ) ) ;
#5593=CARTESIAN_POINT ( 'NONE',  ( 3.200000000000000178, 2.020725942163738686, 3.499999999999999556 ) ) ;
#5616=CARTESIAN_POINT ( 'NONE',  ( 0.2949799022107380542, 0.000000000000000000, 0.000000000000000000 ) ) ;
#5665=ORIENTED_EDGE ( 'NONE', *, *, #4930, .F. ) ;
#5671=EDGE_CURVE ( 'NONE', #1617, #6804, #4036, .T. ) ;
#5673=EDGE_LOOP ( 'NONE', ( #9154, #2546, #3557, #10620 ) ) ;
#5702=CARTESIAN_POINT ( 'NONE',  ( 3.199999999999999734, 0.000000000000000000, 3.499999999999999556 ) ) ;
#5706=FACE_OUTER_BOUND ( 'NONE', #5673, .T. ) ;
#5715=ORIENTED_EDGE ( 'NONE', *, *, #1447, .F. ) ;
#5720=SURFACE_STYLE_USAGE ( .BOTH. , #42 ) ;
#5725=DIRECTION ( 'NONE',  ( 1.000000000000000000, 0.000000000000000000, 0.000000000000000000 ) ) ;
#5729=CARTESIAN_POINT ( 'NONE',  ( 3.319999999999999840, 0.000000000000000000, 3.249999999999998224 ) ) ;
#5732=ORIENTED_EDGE ( 'NONE', *, *, #6288, .T. ) ;
#5747=CARTESIAN_POINT ( 'NONE',  ( 5.791420021395468964, 0.000000000000000000, 3.168237633705329831E-17 ) ) ;
#5771=AXIS2_PLACEMENT_3D ( 'NONE', #9077, #7413, #10915 ) ;
#5797=CARTESIAN_POINT ( 'NONE',  ( 0.02993401039714972331, 3.373851915354646458, 1.156317065392217680 ) ) ;
#5808=EDGE_CURVE ( 'NONE', #1521, #702, #582, .T. ) ;
#5809=ORIENTED_EDGE ( 'NONE', *, *, #3168, .T. ) ;
#5829=ORIENTED_EDGE ( 'NONE', *, *, #10421, .T. ) ;
#5857=CARTESIAN_POINT ( 'NONE',  ( 3.199999999999999734, 3.031088913245550742, 1.749999999999972466 ) ) ;
#5861=EDGE_CURVE ( 'NONE', #8097, #10425, #7479, .T. ) ;
#5865=CARTESIAN_POINT ( 'NONE',  ( 0.000000000000000000, 0.000000000000000000, 0.000000000000000000 ) ) ;
#5871=EDGE_CURVE ( 'NONE', #4949, #3727, #7398, .T. ) ;
#5878=ORIENTED_EDGE ( 'NONE', *, *, #1586, .T. ) ;
#5880=LINE ( 'NONE', #7779, #7519 ) ;
#5884=EDGE_LOOP ( 'NONE', ( #2165, #7160, #4253 ) ) ;
#5895=EDGE_LOOP ( 'NONE', ( #7178, #8575, #6347 ) ) ;
#5897=VECTOR ( 'NONE', #7048, 1000.000000000000000 ) ;
#5907=CARTESIAN_POINT ( 'NONE',  ( 0.2174200650116529521, -2.185595227305000332, 3.214438021527625811 ) ) ;
#5925=CARTESIAN_POINT ( 'NONE',  ( 3.200000000000000178, -2.020725942163647648, 3.499999999999999556 ) ) ;
#5936=( NAMED_UNIT ( * ) PLANE_ANGLE_UNIT ( ) SI_UNIT ( $, .RADIAN. ) );
#5943=DIRECTION ( 'NONE',  ( 0.000000000000000000, 0.000000000000000000, 1.000000000000000000 ) ) ;
#5955=ORIENTED_EDGE ( 'NONE', *, *, #685, .T. ) ;
#5957=DIRECTION ( 'NONE',  ( 1.000000000000000000, -0.000000000000000000, -0.000000000000000000 ) ) ;
#5962=FACE_OUTER_BOUND ( 'NONE', #7379, .T. ) ;
#5965=ORIENTED_EDGE ( 'NONE', *, *, #10813, .T. ) ;
#5969=CIRCLE ( 'NONE', #2241, 3.499999999999999556 ) ;
#5975=FILL_AREA_STYLE_COLOUR ( '', #7410 ) ;
#5982=FACE_OUTER_BOUND ( 'NONE', #8646, .T. ) ;
#5988=EDGE_CURVE ( 'NONE', #4348, #6258, #6334, .T. ) ;
#5996=CARTESIAN_POINT ( 'NONE',  ( 3.170065989602862455, 3.373851915354605602, -1.156317065392272303 ) ) ;
#6006=ORIENTED_EDGE ( 'NONE', *, *, #10319, .F. ) ;
#6031=DIRECTION ( 'NONE',  ( -1.000000000000000000, -0.000000000000000000, -0.000000000000000000 ) ) ;
#6038=EDGE_CURVE ( 'NONE', #10425, #7419, #4936, .T. ) ;
#6044=CARTESIAN_POINT ( 'NONE',  ( 0.3126073911696294338, 2.020725942163657862, -3.499999999999999556 ) ) ;
#6091=DIRECTION ( 'NONE',  ( 0.000000000000000000, 0.8660254037844316022, -0.5000000000000124345 ) ) ;
#6092=DIRECTION ( 'NONE',  ( -1.000000000000000000, -0.000000000000000000, -0.000000000000000000 ) ) ;
#6097=SHAPE_DEFINITION_REPRESENTATION ( #7582, #7975 ) ;
#6104=CYLINDRICAL_SURFACE ( 'NONE', #8919, 2.000000000000000000 ) ;
#6107=ORIENTED_EDGE ( 'NONE', *, *, #8988, .T. ) ;
#6108=DIRECTION ( 'NONE',  ( 1.000000000000000000, 0.000000000000000000, 0.000000000000000000 ) ) ;
#6109=VERTEX_POINT ( 'NONE', #5574 ) ;
#6122=CIRCLE ( 'NONE', #4387, 3.499999999999999556 ) ;
#6129=CIRCLE ( 'NONE', #5771, 3.499999999999997780 ) ;
#6150=DIRECTION ( 'NONE',  ( 0.000000000000000000, 1.000000000000000000, 1.224646799147353207E-16 ) ) ;
#6154=CARTESIAN_POINT ( 'NONE',  ( 4.750000000000000888, 0.000000000000000000, 3.249999999999999112 ) ) ;
#6164=ADVANCED_FACE ( 'NONE', ( #10408 ), #7080, .T. ) ;
#6192=CARTESIAN_POINT ( 'NONE',  ( 0.000000000000000000, 0.000000000000000000, 0.000000000000000000 ) ) ;
#6202=CARTESIAN_POINT ( 'NONE',  ( -1.882954241746308865E-15, 2.859595677584315432, -2.047034997319608252 ) ) ;
#6213=ORIENTED_EDGE ( 'NONE', *, *, #4393, .F. ) ;
#6220=CARTESIAN_POINT ( 'NONE',  ( 3.199999999999999734, -3.031088913245550298, -1.749999999999972911 ) ) ;
#6239=CARTESIAN_POINT ( 'NONE',  ( 0.000000000000000000, 0.000000000000000000, 0.000000000000000000 ) ) ;
#6255=CARTESIAN_POINT ( 'NONE',  ( 0.3126073911696528040, 2.020725942163738686, 3.499999999999999556 ) ) ;
#6258=VERTEX_POINT ( 'NONE', #5729 ) ;
#6272=VERTEX_POINT ( 'NONE', #6555 ) ;
#6286=CIRCLE ( 'NONE', #9300, 3.499999999999999556 ) ;
#6288=EDGE_CURVE ( 'NONE', #6109, #1566, #4304, .T. ) ;
#6295=CARTESIAN_POINT ( 'NONE',  ( 3.199999999999987743, 2.859595677584378937, 2.047034997319559846 ) ) ;
#6313=AXIS2_PLACEMENT_3D ( 'NONE', #2513, #5957, #895 ) ;
#6330=FACE_OUTER_BOUND ( 'NONE', #419, .T. ) ;
#6334=CIRCLE ( 'NONE', #9167, 3.249999999999998224 ) ;
#6347=ORIENTED_EDGE ( 'NONE', *, *, #9398, .T. ) ;
#6351=DIRECTION ( 'NONE',  ( 1.000000000000000000, 0.000000000000000000, 0.000000000000000000 ) ) ;
#6364=CARTESIAN_POINT ( 'NONE',  ( 4.750000000000000888, 0.000000000000000000, 0.000000000000000000 ) ) ;
#6370=FACE_OUTER_BOUND ( 'NONE', #7902, .T. ) ;
#6375=DIRECTION ( 'NONE',  ( -1.000000000000000000, -0.000000000000000000, -0.000000000000000000 ) ) ;
#6407=EDGE_CURVE ( 'NONE', #6258, #4348, #9542, .T. ) ;
#6410=CIRCLE ( 'NONE', #2512, 3.369999999999997886 ) ;
#6434=EDGE_LOOP ( 'NONE', ( #9157, #3753, #5077, #9262, #6556 ) ) ;
#6447=CARTESIAN_POINT ( 'NONE',  ( 3.200000000000000178, 2.020725942163657862, -3.499999999999999556 ) ) ;
#6455=ORIENTED_EDGE ( 'NONE', *, *, #8988, .F. ) ;
#6456=CARTESIAN_POINT ( 'NONE',  ( 2.887392608830354757, -4.041451884327390331, 2.328390191177121598E-14 ) ) ;
#6464=CONICAL_SURFACE ( 'NONE', #10959, 1664.279482350528269, 1.029744258676657198 ) ;
#6505=AXIS2_PLACEMENT_3D ( 'NONE', #6192, #7087, #5419 ) ;
#6509=DIRECTION ( 'NONE',  ( 1.000000000000000000, 0.000000000000000000, 0.000000000000000000 ) ) ;
#6524=CARTESIAN_POINT ( 'NONE',  ( 0.000000000000000000, 0.000000000000000000, 3.249999999999998224 ) ) ;
#6533=FACE_OUTER_BOUND ( 'NONE', #1577, .T. ) ;
#6541=ORIENTED_EDGE ( 'NONE', *, *, #9942, .T. ) ;
#6555=CARTESIAN_POINT ( 'NONE',  ( 0.000000000000000000, 0.000000000000000000, -2.000000000000000000 ) ) ;
#6556=ORIENTED_EDGE ( 'NONE', *, *, #3762, .T. ) ;
#6565=ORIENTED_EDGE ( 'NONE', *, *, #8934, .T. ) ;
#6571=DIRECTION ( 'NONE',  ( -0.5150380749100518241, 0.000000000000000000, 0.8571673007021137769 ) ) ;
#6575=DIRECTION ( 'NONE',  ( 0.000000000000000000, 0.000000000000000000, -1.000000000000000000 ) ) ;
#6583=AXIS2_PLACEMENT_3D ( 'NONE', #5925, #6091, #9313 ) ;
#6605=ORIENTED_EDGE ( 'NONE', *, *, #6038, .F. ) ;
#6622=DIRECTION ( 'NONE',  ( -1.000000000000000000, -0.000000000000000000, -0.000000000000000000 ) ) ;
#6673=B_SPLINE_CURVE_WITH_KNOTS ( 'NONE', 3,
 ( #10834, #3116, #442, #10672, #601, #3896 ),
 .UNSPECIFIED., .F., .F.,
 ( 4, 2, 4 ),
 ( 0.003657268138676097926, 0.004679653797516874353, 0.005702039456357650346 ),
 .UNSPECIFIED. ) ;
#6681=CARTESIAN_POINT ( 'NONE',  ( 3.199999999999999734, 0.000000000000000000, 3.499999999999999556 ) ) ;
#6683=ADVANCED_FACE ( 'NONE', ( #6330 ), #8728, .T. ) ;
#6691=EDGE_CURVE ( 'NONE', #8565, #947, #1894, .T. ) ;
#6712=ORIENTED_EDGE ( 'NONE', *, *, #3077, .T. ) ;
#6756=CARTESIAN_POINT ( 'NONE',  ( 0.000000000000000000, 0.000000000000000000, 0.000000000000000000 ) ) ;
#6790=FACE_BOUND ( 'NONE', #10633, .T. ) ;
#6791=DIRECTION ( 'NONE',  ( -0.000000000000000000, 0.000000000000000000, -1.000000000000000000 ) ) ;
#6792=DIRECTION ( 'NONE',  ( 1.000000000000000000, 0.000000000000000000, 0.000000000000000000 ) ) ;
#6799=ADVANCED_FACE ( 'NONE', ( #3888 ), #7594, .F. ) ;
#6804=VERTEX_POINT ( 'NONE', #8323 ) ;
#6810=CARTESIAN_POINT ( 'NONE',  ( 4.750000000000000888, -3.250000000000000444, -3.980102097228895766E-16 ) ) ;
#6815=VERTEX_POINT ( 'NONE', #4890 ) ;
#6819=ORIENTED_EDGE ( 'NONE', *, *, #2127, .F. ) ;
#6821=CARTESIAN_POINT ( 'NONE',  ( 3.200000000000000178, -0.3416191432522810434, -3.499999999999999112 ) ) ;
#6834=CARTESIAN_POINT ( 'NONE',  ( 0.000000000000000000, 0.000000000000000000, 0.000000000000000000 ) ) ;
#6842=AXIS2_PLACEMENT_3D ( 'NONE', #8969, #2092, #9858 ) ;
#6843=ORIENTED_EDGE ( 'NONE', *, *, #3732, .T. ) ;
#6863=SURFACE_STYLE_FILL_AREA ( #9365 ) ;
#6878=ORIENTED_EDGE ( 'NONE', *, *, #2907, .F. ) ;
#6956=CARTESIAN_POINT ( 'NONE',  ( 0.000000000000000000, 0.000000000000000000, 0.000000000000000000 ) ) ;
#6967=CARTESIAN_POINT ( 'NONE',  ( 0.02539999999999975264, 0.000000000000000000, -2.000000000000000000 ) ) ;
#6985=EDGE_CURVE ( 'NONE', #6272, #4377, #5880, .T. ) ;
#6988=CARTESIAN_POINT ( 'NONE',  ( 4.750000000000000888, -1.622657008870242882E-15, 0.000000000000000000 ) ) ;
#7007=AXIS2_PLACEMENT_3D ( 'NONE', #9467, #3587, #3636 ) ;
#7039=ORIENTED_EDGE ( 'NONE', *, *, #1262, .T. ) ;
#7046=B_SPLINE_CURVE_WITH_KNOTS ( 'NONE', 3,
 ( #3444, #6821, #8549, #4332, #755, #4155 ),
 .UNSPECIFIED., .F., .F.,
 ( 4, 2, 4 ),
 ( 0.01103649464086220618, 0.01205977283736834466, 0.01308305103387448487 ),
 .UNSPECIFIED. ) ;
#7048=DIRECTION ( 'NONE',  ( -1.000000000000000000, -0.000000000000000000, -0.000000000000000000 ) ) ;
#7061=CARTESIAN_POINT ( 'NONE',  ( 0.02539999999999975264, 0.000000000000000000, 0.000000000000000000 ) ) ;
#7067=ORIENTED_EDGE ( 'NONE', *, *, #4536, .T. ) ;
#7078=DIRECTION ( 'NONE',  ( 0.000000000000000000, 0.000000000000000000, 1.000000000000000000 ) ) ;
#7080=CYLINDRICAL_SURFACE ( 'NONE', #1742, 3.249999999999998224 ) ;
#7083=DIRECTION ( 'NONE',  ( 1.000000000000000000, 0.000000000000000000, 0.000000000000000000 ) ) ;
#7087=DIRECTION ( 'NONE',  ( 1.000000000000000000, 0.000000000000000000, 0.000000000000000000 ) ) ;
#7096=EDGE_CURVE ( 'NONE', #4107, #10330, #5198, .T. ) ;
#7104=CARTESIAN_POINT ( 'NONE',  ( 3.200000000000000178, 2.020725942163738686, 3.499999999999999556 ) ) ;
#7114=CARTESIAN_POINT ( 'NONE',  ( 0.2176891316980006652, -1.691919446222015067, 3.500000000000000444 ) ) ;
#7119=ADVANCED_FACE ( 'NONE', ( #2723, #1269 ), #262, .T. ) ;
#7127=VERTEX_POINT ( 'NONE', #6154 ) ;
#7132=CYLINDRICAL_SURFACE ( 'NONE', #4181, 2.000000000000000000 ) ;
#7160=ORIENTED_EDGE ( 'NONE', *, *, #1408, .T. ) ;
#7171=AXIS2_PLACEMENT_3D ( 'NONE', #2365, #8202, #8987 ) ;
#7174=CARTESIAN_POINT ( 'NONE',  ( 0.000000000000000000, 0.000000000000000000, 0.000000000000000000 ) ) ;
#7178=ORIENTED_EDGE ( 'NONE', *, *, #5671, .T. ) ;
#7196=CIRCLE ( 'NONE', #7551, 3.499999999999999556 ) ;
#7204=CARTESIAN_POINT ( 'NONE',  ( 3.200000000000001510, 2.686816014504541439, -2.346298152288397443 ) ) ;
#7231=AXIS2_PLACEMENT_3D ( 'NONE', #9784, #5725, #7330 ) ;
#7241=CARTESIAN_POINT ( 'NONE',  ( 0.2182762428107514474, 1.693953258775869442, 3.499999999999999556 ) ) ;
#7243=CARTESIAN_POINT ( 'NONE',  ( 2.887392608830845031, -2.020725942164465661, -3.499999999999999556 ) ) ;
#7249=CIRCLE ( 'NONE', #152, 3.249999999999999556 ) ;
#7264=ORIENTED_EDGE ( 'NONE', *, *, #7627, .T. ) ;
#7272=EDGE_LOOP ( 'NONE', ( #5145, #7637, #8678, #1027, #95, #8199 ) ) ;
#7289=CARTESIAN_POINT ( 'NONE',  ( 0.000000000000000000, 0.000000000000000000, 3.499999999999999556 ) ) ;
#7301=CARTESIAN_POINT ( 'NONE',  ( 3.200000000000000178, 0.000000000000000000, 0.000000000000000000 ) ) ;
#7330=DIRECTION ( 'NONE',  ( 0.000000000000000000, 0.000000000000000000, -1.000000000000000000 ) ) ;
#7336=ORIENTED_EDGE ( 'NONE', *, *, #5298, .T. ) ;
#7340=DIRECTION ( 'NONE',  ( 0.000000000000000000, 0.000000000000000000, -1.000000000000000000 ) ) ;
#7342=DIRECTION ( 'NONE',  ( -1.000000000000000000, -0.000000000000000000, -0.000000000000000000 ) ) ;
#7344=ADVANCED_FACE ( 'NONE', ( #5706 ), #1319, .F. ) ;
#7356=CIRCLE ( 'NONE', #8784, 3.499999999999997780 ) ;
#7378=CARTESIAN_POINT ( 'NONE',  ( 3.199999999999992628, -2.859595677584409135, -2.047034997319491900 ) ) ;
#7379=EDGE_LOOP ( 'NONE', ( #986, #1352, #4750, #2903, #7336, #8392 ) ) ;
#7398=CIRCLE ( 'NONE', #8649, 1.650000000000000355 ) ;
#7399=CIRCLE ( 'NONE', #6505, 2.000000000000000000 ) ;
#7404=ORIENTED_EDGE ( 'NONE', *, *, #4841, .T. ) ;
#7409=CARTESIAN_POINT ( 'NONE',  ( 3.319999999999999840, 0.000000000000000000, 0.000000000000000000 ) ) ;
#7410=COLOUR_RGB ( '', 0.09019608, 0.27058824, 0.51372549) ;
#7413=DIRECTION ( 'NONE',  ( 1.000000000000000000, 0.000000000000000000, 0.000000000000000000 ) ) ;
#7416=CARTESIAN_POINT ( 'NONE',  ( 2.887392608830354757, -4.041451884327390331, 2.328390191177121598E-14 ) ) ;
#7419=VERTEX_POINT ( 'NONE', #10812 ) ;
#7461=CARTESIAN_POINT ( 'NONE',  ( 2.887392608830347207, 2.020725942163738686, 3.499999999999999556 ) ) ;
#7473=AXIS2_PLACEMENT_3D ( 'NONE', #4185, #7342, #9175 ) ;
#7479=B_SPLINE_CURVE_WITH_KNOTS ( 'NONE', 3,
 ( #7461, #1576, #4975, #8348, #3300, #6681 ),
 .UNSPECIFIED., .F., .F.,
 ( 4, 2, 4 ),
 ( 0.008988604078116378682, 0.01001254935948934707, 0.01103649464086231546 ),
 .UNSPECIFIED. ) ;
#7493=ORIENTED_EDGE ( 'NONE', *, *, #4200, .T. ) ;
#7517=ORIENTED_EDGE ( 'NONE', *, *, #8232, .T. ) ;
#7519=VECTOR ( 'NONE', #97, 1000.000000000000000 ) ;
#7546=EDGE_LOOP ( 'NONE', ( #1645, #10948, #8710, #8011, #6006, #9941 ) ) ;
#7551=AXIS2_PLACEMENT_3D ( 'NONE', #10474, #5416, #2920 ) ;
#7574=PRODUCT_DEFINITION_FORMATION_WITH_SPECIFIED_SOURCE ( 'ANY', '', #5016, .NOT_KNOWN. ) ;
#7582=PRODUCT_DEFINITION_SHAPE ( 'NONE', 'NONE',  #3420 ) ;
#7591=DIRECTION ( 'NONE',  ( 0.000000000000000000, 0.000000000000000000, -1.000000000000000000 ) ) ;
#7594=CONICAL_SURFACE ( 'NONE', #791, 1.615000000000000213, 0.9599310885968811435 ) ;
#7599=CYLINDRICAL_SURFACE ( 'NONE', #3468, 1.650000000000000355 ) ;
#7614=CARTESIAN_POINT ( 'NONE',  ( 2.982579934988239145, 3.876582599186223277, -0.2855619784720935250 ) ) ;
#7623=DIRECTION ( 'NONE',  ( 0.000000000000000000, 0.000000000000000000, -1.000000000000000000 ) ) ;
#7627=EDGE_CURVE ( 'NONE', #10425, #4665, #6286, .T. ) ;
#7633=CARTESIAN_POINT ( 'NONE',  ( 0.000000000000000000, 0.000000000000000000, 0.000000000000000000 ) ) ;
#7637=ORIENTED_EDGE ( 'NONE', *, *, #1388, .T. ) ;
#7646=DIRECTION ( 'NONE',  ( 0.000000000000000000, 0.000000000000000000, 1.000000000000000000 ) ) ;
#7671=CARTESIAN_POINT ( 'NONE',  ( 0.000000000000000000, -3.031088913245550298, -1.749999999999972911 ) ) ;
#7704=DIRECTION ( 'NONE',  ( 0.000000000000000000, 0.000000000000000000, 1.000000000000000000 ) ) ;
#7721=CARTESIAN_POINT ( 'NONE',  ( 0.000000000000000000, 0.000000000000000000, 0.000000000000000000 ) ) ;
#7733=FACE_OUTER_BOUND ( 'NONE', #9435, .T. ) ;
#7740=B_SPLINE_CURVE_WITH_KNOTS ( 'NONE', 3,
 ( #2978, #3692, #5361, #7972 ),
 .UNSPECIFIED., .F., .F.,
 ( 4, 4 ),
 ( 2.380739286522876005E-07, 0.002044882221487540584 ),
 .UNSPECIFIED. ) ;
#7766=AXIS2_PLACEMENT_3D ( 'NONE', #1013, #6792, #2519 ) ;
#7767=MECHANICAL_DESIGN_GEOMETRIC_PRESENTATION_REPRESENTATION('',(#2799),#8281);
#7778=ORIENTED_EDGE ( 'NONE', *, *, #1460, .T. ) ;
#7779=CARTESIAN_POINT ( 'NONE',  ( 0.000000000000000000, 0.000000000000000000, -2.000000000000000000 ) ) ;
#7802=ADVANCED_FACE ( 'NONE', ( #10936 ), #8948, .T. ) ;
#7807=CARTESIAN_POINT ( 'NONE',  ( 5.791420021395468964, 3.879972077055416885E-33, -3.168237633705329831E-17 ) ) ;
#7811=EDGE_CURVE ( 'NONE', #1566, #1959, #7046, .T. ) ;
#7853=DIRECTION ( 'NONE',  ( -1.000000000000000000, 0.000000000000000000, 0.000000000000000000 ) ) ;
#7859=EDGE_CURVE ( 'NONE', #3727, #4949, #9661, .T. ) ;
#7872=CARTESIAN_POINT ( 'NONE',  ( 3.199999999999999734, -3.031088913245509886, 1.750000000000043077 ) ) ;
#7885=DIRECTION ( 'NONE',  ( 0.000000000000000000, 0.000000000000000000, -1.000000000000000000 ) ) ;
#7894=CARTESIAN_POINT ( 'NONE',  ( 0.000000000000000000, 0.000000000000000000, 3.499999999999999556 ) ) ;
#7902=EDGE_LOOP ( 'NONE', ( #8943, #1891, #5050, #2066 ) ) ;
#7911=AXIS2_PLACEMENT_3D ( 'NONE', #181, #6791, #3578 ) ;
#7916=ORIENTED_EDGE ( 'NONE', *, *, #3348, .F. ) ;
#7921=CARTESIAN_POINT ( 'NONE',  ( 3.199999999999987743, 3.375361811986532068, 1.153701847711613215 ) ) ;
#7923=AXIS2_PLACEMENT_3D ( 'NONE', #2422, #3428, #6575 ) ;
#7942=DIRECTION ( 'NONE',  ( 0.000000000000000000, 0.000000000000000000, 1.000000000000000000 ) ) ;
#7943=ORIENTED_EDGE ( 'NONE', *, *, #6038, .T. ) ;
#7944=ADVANCED_FACE ( 'NONE', ( #9548 ), #3717, .F. ) ;
#7972=CARTESIAN_POINT ( 'NONE',  ( 0.000000000000000000, -3.031088913245550298, -1.749999999999972911 ) ) ;
#7975=SHAPE_REPRESENTATION ( 'domed cap nut_din_DIN 1587 - M4 --NNU', ( #308 ), #8995 ) ;
#7976=CARTESIAN_POINT ( 'NONE',  ( 0.3126073911696528040, 2.020725942163738686, 3.499999999999999556 ) ) ;
#7999=CARTESIAN_POINT ( 'NONE',  ( 4.800000000000000711, 0.000000000000000000, 0.000000000000000000 ) ) ;
#8011=ORIENTED_EDGE ( 'NONE', *, *, #4667, .F. ) ;
#8028=PRESENTATION_STYLE_ASSIGNMENT (( #5365 ) ) ;
#8042=LINE ( 'NONE', #6524, #10398 ) ;
#8043=VERTEX_POINT ( 'NONE', #2760 ) ;
#8053=CARTESIAN_POINT ( 'NONE',  ( 4.750000000000000888, -1.622657008870242882E-15, 0.000000000000000000 ) ) ;
#8054=ORIENTED_EDGE ( 'NONE', *, *, #5808, .F. ) ;
#8072=DIRECTION ( 'NONE',  ( 1.000000000000000000, 0.000000000000000000, 0.000000000000000000 ) ) ;
#8094=CARTESIAN_POINT ( 'NONE',  ( 2.982310868302101792, -1.691919446221600731, 3.499999999999999556 ) ) ;
#8097=VERTEX_POINT ( 'NONE', #913 ) ;
#8122=AXIS2_PLACEMENT_3D ( 'NONE', #9015, #6108, #7623 ) ;
#8125=B_SPLINE_CURVE_WITH_KNOTS ( 'NONE', 3,
 ( #10383, #8669, #5996, #991, #7614, #3558 ),
 .UNSPECIFIED., .F., .F.,
 ( 4, 2, 4 ),
 ( 0.002044882221487493313, 0.003063384235218477233, 0.004081886248949461587 ),
 .UNSPECIFIED. ) ;
#8128=ADVANCED_FACE ( 'NONE', ( #10363 ), #3287, .T. ) ;
#8134=APPLICATION_CONTEXT ( 'automotive_design' ) ;
#8155=ORIENTED_EDGE ( 'NONE', *, *, #5502, .F. ) ;
#8160=VERTEX_POINT ( 'NONE', #3369 ) ;
#8165=DIRECTION ( 'NONE',  ( -1.000000000000000000, -0.000000000000000000, -0.000000000000000000 ) ) ;
#8181=CARTESIAN_POINT ( 'NONE',  ( 0.3126073911696294338, 2.020725942163657862, -3.499999999999999556 ) ) ;
#8190=CONICAL_SURFACE ( 'NONE', #2700, 4.624785217660733139, 1.047197551196604071 ) ;
#8199=ORIENTED_EDGE ( 'NONE', *, *, #10813, .F. ) ;
#8202=DIRECTION ( 'NONE',  ( -1.000000000000000000, -0.000000000000000000, -0.000000000000000000 ) ) ;
#8212=ORIENTED_EDGE ( 'NONE', *, *, #9770, .T. ) ;
#8232=EDGE_CURVE ( 'NONE', #2863, #3414, #8125, .T. ) ;
#8240=B_SPLINE_CURVE_WITH_KNOTS ( 'NONE', 3,
 ( #9428, #3655, #7204, #1265 ),
 .UNSPECIFIED., .F., .F.,
 ( 4, 4 ),
 ( 2.380739282171252709E-07, 0.002044882221487493313 ),
 .UNSPECIFIED. ) ;
#8247=DIRECTION ( 'NONE',  ( -1.000000000000000000, -0.000000000000000000, -0.000000000000000000 ) ) ;
#8267=ORIENTED_EDGE ( 'NONE', *, *, #6288, .F. ) ;
#8281=( GEOMETRIC_REPRESENTATION_CONTEXT ( 3 ) GLOBAL_UNCERTAINTY_ASSIGNED_CONTEXT ( ( #2769 ) ) GLOBAL_UNIT_ASSIGNED_CONTEXT ( ( #10761, #3213, #8379 ) ) REPRESENTATION_CONTEXT ( 'NONE', 'WORKASPACE' ) );
#8300=LINE ( 'NONE', #9921, #3999 ) ;
#8323=CARTESIAN_POINT ( 'NONE',  ( 0.000000000000000000, -3.031088913245509886, 1.750000000000043077 ) ) ;
#8330=CARTESIAN_POINT ( 'NONE',  ( 2.982579934988244030, -3.876582599186213063, 0.2855619784720940246 ) ) ;
#8348=CARTESIAN_POINT ( 'NONE',  ( 3.169801662054985592, 0.6882444255504213126, 3.499999999999999556 ) ) ;
#8364=EDGE_CURVE ( 'NONE', #1566, #2863, #7356, .T. ) ;
#8379=( NAMED_UNIT ( * ) SI_UNIT ( $, .STERADIAN. ) SOLID_ANGLE_UNIT ( ) );
#8389=DIRECTION ( 'NONE',  ( 0.000000000000000000, 0.000000000000000000, -1.000000000000000000 ) ) ;
#8392=ORIENTED_EDGE ( 'NONE', *, *, #685, .F. ) ;
#8420=VECTOR ( 'NONE', #9878, 1000.000000000000000 ) ;
#8427=TOROIDAL_SURFACE ( 'NONE', #4719, 3.369999999999997886, 0.1199999999999999956 ) ;
#8437=EDGE_LOOP ( 'NONE', ( #5878, #2340, #6605 ) ) ;
#8449=AXIS2_PLACEMENT_3D ( 'NONE', #8, #10185, #2580 ) ;
#8451=ORIENTED_EDGE ( 'NONE', *, *, #8364, .F. ) ;
#8464=DIRECTION ( 'NONE',  ( -0.5150380749100518241, 1.049727191138620421E-16, -0.8571673007021137769 ) ) ;
#8477=FACE_OUTER_BOUND ( 'NONE', #82, .T. ) ;
#8490=ORIENTED_EDGE ( 'NONE', *, *, #9812, .T. ) ;
#8493=DIRECTION ( 'NONE',  ( 0.000000000000000000, 0.000000000000000000, -1.000000000000000000 ) ) ;
#8527=ORIENTED_EDGE ( 'NONE', *, *, #7096, .F. ) ;
#8537=CARTESIAN_POINT ( 'NONE',  ( 2.887392608830372964, -2.020725942163647648, 3.499999999999999556 ) ) ;
#8549=CARTESIAN_POINT ( 'NONE',  ( 3.170625919164804518, -0.6808742863896959374, -3.500000000000000000 ) ) ;
#8565=VERTEX_POINT ( 'NONE', #4778 ) ;
#8575=ORIENTED_EDGE ( 'NONE', *, *, #10041, .T. ) ;
#8584=EDGE_CURVE ( 'NONE', #6109, #10330, #3150, .T. ) ;
#8595=ADVANCED_FACE ( 'NONE', ( #6533 ), #6464, .F. ) ;
#8646=EDGE_LOOP ( 'NONE', ( #5715, #365, #7778, #4947 ) ) ;
#8649=AXIS2_PLACEMENT_3D ( 'NONE', #4859, #9235, #1418 ) ;
#8652=UNCERTAINTY_MEASURE_WITH_UNIT (LENGTH_MEASURE( 1.000000000000000082E-05 ), #10773, 'distance_accuracy_value', 'NONE');
#8657=PLANE ( 'NONE',  #6583 ) ;
#8661=ORIENTED_EDGE ( 'NONE', *, *, #158, .T. ) ;
#8669=CARTESIAN_POINT ( 'NONE',  ( 3.200000000000000622, 3.202582148906713222, -1.452965002680467910 ) ) ;
#8678=ORIENTED_EDGE ( 'NONE', *, *, #131, .F. ) ;
#8680=ORIENTED_EDGE ( 'NONE', *, *, #5808, .T. ) ;
#8688=DIRECTION ( 'NONE',  ( 0.000000000000000000, 0.000000000000000000, 1.000000000000000000 ) ) ;
#8706=CARTESIAN_POINT ( 'NONE',  ( 0.2704726383733979667, 0.000000000000000000, 1.650000000000000355 ) ) ;
#8710=ORIENTED_EDGE ( 'NONE', *, *, #9770, .F. ) ;
#8715=PRODUCT_CONTEXT ( 'NONE', #8134, 'mechanical' ) ;
#8723=EDGE_CURVE ( 'NONE', #4377, #3105, #10013, .T. ) ;
#8725=CIRCLE ( 'NONE', #5359, 3.250000000000000000 ) ;
#8728=SPHERICAL_SURFACE ( 'NONE', #3865, 3.250000000000000000 ) ;
#8731=EDGE_LOOP ( 'NONE', ( #2011, #172, #5809, #9237, #8885 ) ) ;
#8739=VERTEX_POINT ( 'NONE', #8706 ) ;
#8748=( NAMED_UNIT ( * ) PLANE_ANGLE_UNIT ( ) SI_UNIT ( $, .RADIAN. ) );
#8752=ORIENTED_EDGE ( 'NONE', *, *, #9942, .F. ) ;
#8758=CARTESIAN_POINT ( 'NONE',  ( 0.2174200650117457945, 2.185595227304829802, -3.214438021527938893 ) ) ;
#8763=EDGE_LOOP ( 'NONE', ( #4192, #8752, #7517 ) ) ;
#8765=APPLICATION_CONTEXT ( 'automotive_design' ) ;
#8774=ORIENTED_EDGE ( 'NONE', *, *, #2830, .F. ) ;
#8776=ORIENTED_EDGE ( 'NONE', *, *, #7096, .T. ) ;
#8777=DIRECTION ( 'NONE',  ( 0.000000000000000000, 1.000000000000000000, 0.000000000000000000 ) ) ;
#8784=AXIS2_PLACEMENT_3D ( 'NONE', #9715, #2052, #2843 ) ;
#8799=CARTESIAN_POINT ( 'NONE',  ( 0.000000000000000000, 0.000000000000000000, 0.000000000000000000 ) ) ;
#8827=ORIENTED_EDGE ( 'NONE', *, *, #10990, .T. ) ;
#8853=DIRECTION ( 'NONE',  ( -1.000000000000000000, -0.000000000000000000, -0.000000000000000000 ) ) ;
#8856=ORIENTED_EDGE ( 'NONE', *, *, #981, .T. ) ;
#8881=DIRECTION ( 'NONE',  ( -1.000000000000000000, -0.000000000000000000, -0.000000000000000000 ) ) ;
#8885=ORIENTED_EDGE ( 'NONE', *, *, #6407, .T. ) ;
#8904=VERTEX_POINT ( 'NONE', #520 ) ;
#8919=AXIS2_PLACEMENT_3D ( 'NONE', #6834, #9499, #50 ) ;
#8934=EDGE_CURVE ( 'NONE', #3990, #4107, #3809, .T. ) ;
#8943=ORIENTED_EDGE ( 'NONE', *, *, #623, .F. ) ;
#8948=CONICAL_SURFACE ( 'NONE', #3464, 3.499999999999999556, 1.047197551196603849 ) ;
#8964=CARTESIAN_POINT ( 'NONE',  ( -1.524659305057740610E-17, 0.3418418480469876952, 3.499999999999999556 ) ) ;
#8966=FACE_OUTER_BOUND ( 'NONE', #8437, .T. ) ;
#8969=CARTESIAN_POINT ( 'NONE',  ( 2.550604951803072673, 0.000000000000000000, 0.000000000000000000 ) ) ;
#8971=EDGE_LOOP ( 'NONE', ( #7493, #928, #5955 ) ) ;
#8972=CARTESIAN_POINT ( 'NONE',  ( -6.663765011382338240E-15, -3.375361811986485439, 1.153701847711662287 ) ) ;
#8983=CARTESIAN_POINT ( 'NONE',  ( 4.750000000000000888, 0.000000000000000000, 0.000000000000000000 ) ) ;
#8987=DIRECTION ( 'NONE',  ( 0.000000000000000000, 0.000000000000000000, 1.000000000000000000 ) ) ;
#8988=EDGE_CURVE ( 'NONE', #10050, #3990, #7740, .T. ) ;
#8995=( GEOMETRIC_REPRESENTATION_CONTEXT ( 3 ) GLOBAL_UNCERTAINTY_ASSIGNED_CONTEXT ( ( #8652 ) ) GLOBAL_UNIT_ASSIGNED_CONTEXT ( ( #10773, #5936, #9213 ) ) REPRESENTATION_CONTEXT ( 'NONE', 'WORKASPACE' ) );
#9015=CARTESIAN_POINT ( 'NONE',  ( 3.319999999999999840, 0.000000000000000000, 0.000000000000000000 ) ) ;
#9035=DIRECTION ( 'NONE',  ( 0.000000000000000000, 0.000000000000000000, -1.000000000000000000 ) ) ;
#9036=DIRECTION ( 'NONE',  ( 0.000000000000000000, 0.000000000000000000, -1.000000000000000000 ) ) ;
#9047=DIRECTION ( 'NONE',  ( -1.000000000000000000, 0.000000000000000000, 0.000000000000000000 ) ) ;
#9052=EDGE_CURVE ( 'NONE', #4348, #58, #10374, .T. ) ;
#9058=CARTESIAN_POINT ( 'NONE',  ( 3.200000000000000178, 0.3418418480469731513, -3.499999999999999556 ) ) ;
#9077=CARTESIAN_POINT ( 'NONE',  ( 3.200000000000000178, 0.000000000000000000, 0.000000000000000000 ) ) ;
#9102=CARTESIAN_POINT ( 'NONE',  ( 0.000000000000000000, 0.000000000000000000, 0.000000000000000000 ) ) ;
#9107=CARTESIAN_POINT ( 'NONE',  ( 2.981723757189264301, 1.693953258775802162, -3.499999999999999112 ) ) ;
#9111=ADVANCED_FACE ( 'NONE', ( #2383 ), #4169, .T. ) ;
#9120=AXIS2_PLACEMENT_3D ( 'NONE', #7999, #10379, #7942 ) ;
#9125=CARTESIAN_POINT ( 'NONE',  ( 3.200000000000000178, 0.000000000000000000, 0.000000000000000000 ) ) ;
#9133=CARTESIAN_POINT ( 'NONE',  ( -994.2085799786045754, 0.000000000000000000, 0.000000000000000000 ) ) ;
#9154=ORIENTED_EDGE ( 'NONE', *, *, #7859, .F. ) ;
#9157=ORIENTED_EDGE ( 'NONE', *, *, #5551, .T. ) ;
#9160=CARTESIAN_POINT ( 'NONE',  ( 2.887392608830354757, -4.041451884327390331, 2.328390191177121598E-14 ) ) ;
#9164=CARTESIAN_POINT ( 'NONE',  ( 2.887392608830370744, 2.020725942163657862, -3.499999999999999556 ) ) ;
#9167=AXIS2_PLACEMENT_3D ( 'NONE', #5086, #901, #956 ) ;
#9175=DIRECTION ( 'NONE',  ( 0.000000000000000000, 0.000000000000000000, 1.000000000000000000 ) ) ;
#9186=CARTESIAN_POINT ( 'NONE',  ( 0.2174200650117649736, 3.876582599186232603, 0.2855619784720455634 ) ) ;
#9197=ORIENTED_EDGE ( 'NONE', *, *, #4200, .F. ) ;
#9210=B_SPLINE_CURVE_WITH_KNOTS ( 'NONE', 3,
 ( #588, #7378, #3935, #3156, #9987, #428 ),
 .UNSPECIFIED., .F., .F.,
 ( 4, 2, 4 ),
 ( 0.002044882221487522803, 0.003063384235218269934, 0.004081886248949017498 ),
 .UNSPECIFIED. ) ;
#9213=( NAMED_UNIT ( * ) SI_UNIT ( $, .STERADIAN. ) SOLID_ANGLE_UNIT ( ) );
#9231=CARTESIAN_POINT ( 'NONE',  ( 2.982579934988233372, 2.185595227304907073, 3.214438021527930012 ) ) ;
#9235=DIRECTION ( 'NONE',  ( -1.000000000000000000, -0.000000000000000000, -0.000000000000000000 ) ) ;
#9237=ORIENTED_EDGE ( 'NONE', *, *, #3161, .T. ) ;
#9246=CARTESIAN_POINT ( 'NONE',  ( 0.3126073911696448659, -4.041451884327390331, 2.328673539876467720E-14 ) ) ;
#9248=CIRCLE ( 'NONE', #7473, 3.249999999999998668 ) ;
#9259=AXIS2_PLACEMENT_3D ( 'NONE', #7061, #995, #4404 ) ;
#9262=ORIENTED_EDGE ( 'NONE', *, *, #3161, .F. ) ;
#9264=ORIENTED_EDGE ( 'NONE', *, *, #8364, .T. ) ;
#9271=CIRCLE ( 'NONE', #2536, 0.1199999999999998845 ) ;
#9289=PLANE ( 'NONE',  #804 ) ;
#9295=CARTESIAN_POINT ( 'NONE',  ( 0.1217565302851138787, 3.710888496608923948, -0.5725525826504940241 ) ) ;
#9300=AXIS2_PLACEMENT_3D ( 'NONE', #4892, #8165, #3059 ) ;
#9303=CARTESIAN_POINT ( 'NONE',  ( 0.000000000000000000, 2.449293598294706414E-16, 2.000000000000000000 ) ) ;
#9313=DIRECTION ( 'NONE',  ( 0.000000000000000000, 0.5000000000000123235, 0.8660254037844314912 ) ) ;
#9316=ORIENTED_EDGE ( 'NONE', *, *, #5861, .F. ) ;
#9337=AXIS2_PLACEMENT_3D ( 'NONE', #6364, #9752, #2143 ) ;
#9346=DIRECTION ( 'NONE',  ( -1.000000000000000000, -0.000000000000000000, -0.000000000000000000 ) ) ;
#9351=CARTESIAN_POINT ( 'NONE',  ( 0.000000000000000000, 2.020725942163738686, 3.499999999999999556 ) ) ;
#9354=ORIENTED_EDGE ( 'NONE', *, *, #3732, .F. ) ;
#9356=B_SPLINE_CURVE_WITH_KNOTS ( 'NONE', 3,
 ( #1244, #10525, #7921, #5413 ),
 .UNSPECIFIED., .F., .F.,
 ( 4, 4 ),
 ( 2.380739282170373118E-07, 0.002044882221487527140 ),
 .UNSPECIFIED. ) ;
#9365=FILL_AREA_STYLE ('',( #5975 ) ) ;
#9370=MECHANICAL_DESIGN_GEOMETRIC_PRESENTATION_REPRESENTATION('',(#3164),#3525);
#9374=AXIS2_PLACEMENT_3D ( 'NONE', #5518, #8853, #7078 ) ;
#9380=CARTESIAN_POINT ( 'NONE',  ( 7.623296525288699970E-18, 0.3418418480469747056, -3.499999999999999112 ) ) ;
#9392=ORIENTED_EDGE ( 'NONE', *, *, #5502, .T. ) ;
#9396=ORIENTED_EDGE ( 'NONE', *, *, #10641, .F. ) ;
#9398=EDGE_CURVE ( 'NONE', #3990, #1617, #1524, .T. ) ;
#9428=CARTESIAN_POINT ( 'NONE',  ( 2.887392608830370744, 2.020725942163657862, -3.499999999999999556 ) ) ;
#9435=EDGE_LOOP ( 'NONE', ( #4974, #8212, #8527 ) ) ;
#9467=CARTESIAN_POINT ( 'NONE',  ( 3.319999999999999840, 0.000000000000000000, -3.369999999999997886 ) ) ;
#9486=VERTEX_POINT ( 'NONE', #6810 ) ;
#9499=DIRECTION ( 'NONE',  ( 1.000000000000000000, -0.000000000000000000, -0.000000000000000000 ) ) ;
#9505=ORIENTED_EDGE ( 'NONE', *, *, #8584, .F. ) ;
#9507=CONICAL_SURFACE ( 'NONE', #2950, 3.499999999999999556, 1.047197551196603849 ) ;
#9508=ORIENTED_EDGE ( 'NONE', *, *, #9877, .T. ) ;
#9542=CIRCLE ( 'NONE', #8122, 3.249999999999998224 ) ;
#9544=FACE_OUTER_BOUND ( 'NONE', #10616, .T. ) ;
#9548=FACE_OUTER_BOUND ( 'NONE', #10210, .T. ) ;
#9565=DIRECTION ( 'NONE',  ( 1.000000000000000000, 0.000000000000000000, 0.000000000000000000 ) ) ;
#9582=ORIENTED_EDGE ( 'NONE', *, *, #4163, .F. ) ;
#9589=LINE ( 'NONE', #1990, #10158 ) ;
#9590=CARTESIAN_POINT ( 'NONE',  ( 3.200000000000000178, 0.000000000000000000, 0.000000000000000000 ) ) ;
#9605=ADVANCED_FACE ( 'NONE', ( #5982 ), #7599, .F. ) ;
#9648=CARTESIAN_POINT ( 'NONE',  ( 1.159276027961613812E-14, 2.686816014504609829, 2.346298152288358363 ) ) ;
#9661=CIRCLE ( 'NONE', #9120, 1.650000000000000355 ) ;
#9666=DIRECTION ( 'NONE',  ( -0.000000000000000000, 0.000000000000000000, -1.000000000000000000 ) ) ;
#9676=B_SPLINE_CURVE_WITH_KNOTS ( 'NONE', 3,
 ( #2922, #6295, #9693, #2086, #9231, #10075 ),
 .UNSPECIFIED., .F., .F.,
 ( 4, 2, 4 ),
 ( 0.002044882221487527140, 0.003063384235218493713, 0.004081886248949459853 ),
 .UNSPECIFIED. ) ;
#9693=CARTESIAN_POINT ( 'NONE',  ( 3.170065989602850909, 2.688325911136496771, 2.343682934607755008 ) ) ;
#9694=CARTESIAN_POINT ( 'NONE',  ( 0.000000000000000000, 2.449293598294706414E-16, 2.000000000000000000 ) ) ;
#9707=LINE ( 'NONE', #4713, #1639 ) ;
#9715=CARTESIAN_POINT ( 'NONE',  ( 3.200000000000000178, 0.000000000000000000, 0.000000000000000000 ) ) ;
#9752=DIRECTION ( 'NONE',  ( -1.000000000000000000, -0.000000000000000000, -0.000000000000000000 ) ) ;
#9758=DIRECTION ( 'NONE',  ( 0.000000000000000000, 0.000000000000000000, -1.000000000000000000 ) ) ;
#9770=EDGE_CURVE ( 'NONE', #8160, #10330, #853, .T. ) ;
#9772=CARTESIAN_POINT ( 'NONE',  ( 0.02993401039714445322, -3.373851915354637576, -1.156317065392215238 ) ) ;
#9784=CARTESIAN_POINT ( 'NONE',  ( 3.319999999999999840, 0.000000000000000000, 0.000000000000000000 ) ) ;
#9792=ORIENTED_EDGE ( 'NONE', *, *, #7811, .T. ) ;
#9808=AXIS2_PLACEMENT_3D ( 'NONE', #3877, #10702, #3565 ) ;
#9812=EDGE_CURVE ( 'NONE', #2901, #4949, #10029, .T. ) ;
#9858=DIRECTION ( 'NONE',  ( 0.000000000000000000, 0.000000000000000000, 1.000000000000000000 ) ) ;
#9862=ORIENTED_EDGE ( 'NONE', *, *, #10957, .F. ) ;
#9870=CARTESIAN_POINT ( 'NONE',  ( 0.000000000000000000, 0.000000000000000000, 0.000000000000000000 ) ) ;
#9877=EDGE_CURVE ( 'NONE', #8097, #10875, #10745, .T. ) ;
#9878=DIRECTION ( 'NONE',  ( -1.000000000000000000, -0.000000000000000000, -0.000000000000000000 ) ) ;
#9892=ORIENTED_EDGE ( 'NONE', *, *, #4860, .T. ) ;
#9906=EDGE_CURVE ( 'NONE', #1521, #1617, #8300, .T. ) ;
#9917=ORIENTED_EDGE ( 'NONE', *, *, #3348, .T. ) ;
#9921=CARTESIAN_POINT ( 'NONE',  ( 3.200000000000000178, -4.041451884327390331, 2.328587628042611615E-14 ) ) ;
#9925=DIRECTION ( 'NONE',  ( -1.000000000000000000, -0.000000000000000000, -0.000000000000000000 ) ) ;
#9930=CARTESIAN_POINT ( 'NONE',  ( -994.2085799786045754, 0.000000000000000000, 0.000000000000000000 ) ) ;
#9941=ORIENTED_EDGE ( 'NONE', *, *, #8232, .F. ) ;
#9942=EDGE_CURVE ( 'NONE', #2863, #4665, #6129, .T. ) ;
#9965=ORIENTED_EDGE ( 'NONE', *, *, #8723, .T. ) ;
#9975=CARTESIAN_POINT ( 'NONE',  ( 3.061857526609965685, -1.355358988605187998, 3.499999999999999556 ) ) ;
#9987=CARTESIAN_POINT ( 'NONE',  ( 2.982579934988325743, -2.185595227305077604, -3.214438021527616929 ) ) ;
#10013=CIRCLE ( 'NONE', #3637, 2.000000000000000000 ) ;
#10014=CLOSED_SHELL ( 'NONE', ( #10635, #7344, #8595, #6799, #915, #1751, #165, #7119, #6683, #6164, #10814, #3716, #2752, #10426, #5348, #1658, #3910, #10294, #7944, #1256, #3895, #488, #8128, #7802, #3149, #9111, #1572, #608, #3928, #10080, #1005, #2418, #9605, #4571 ) ) ;
#10016=DIRECTION ( 'NONE',  ( -1.000000000000000000, 0.000000000000000000, -0.000000000000000000 ) ) ;
#10019=CARTESIAN_POINT ( 'NONE',  ( 3.078243469714883940, -3.710888496608934606, -0.5725525826504437310 ) ) ;
#10022=DIRECTION ( 'NONE',  ( 1.000000000000000000, 0.000000000000000000, 0.000000000000000000 ) ) ;
#10029=LINE ( 'NONE', #5747, #1881 ) ;
#10041=EDGE_CURVE ( 'NONE', #6804, #3990, #7196, .T. ) ;
#10050=VERTEX_POINT ( 'NONE', #2867 ) ;
#10059=DIRECTION ( 'NONE',  ( -0.5735764363510461594, 0.000000000000000000, 0.8191520442889916875 ) ) ;
#10062=CARTESIAN_POINT ( 'NONE',  ( 3.319999999999999840, 4.127059713126577826E-16, 3.369999999999997886 ) ) ;
#10063=VERTEX_POINT ( 'NONE', #1185 ) ;
#10068=VERTEX_POINT ( 'NONE', #4695 ) ;
#10075=CARTESIAN_POINT ( 'NONE',  ( 2.887392608830347207, 2.020725942163738686, 3.499999999999999556 ) ) ;
#10080=ADVANCED_FACE ( 'NONE', ( #10360 ), #7132, .F. ) ;
#10081=EDGE_LOOP ( 'NONE', ( #9392, #10179, #9582 ) ) ;
#10087=CARTESIAN_POINT ( 'NONE',  ( 0.000000000000000000, 0.000000000000000000, 0.000000000000000000 ) ) ;
#10091=FACE_OUTER_BOUND ( 'NONE', #6434, .T. ) ;
#10095=ORIENTED_EDGE ( 'NONE', *, *, #5861, .T. ) ;
#10118=DIRECTION ( 'NONE',  ( 1.000000000000000000, 0.000000000000000000, 0.000000000000000000 ) ) ;
#10133=B_SPLINE_CURVE_WITH_KNOTS ( 'NONE', 3,
 ( #3411, #4361, #2469, #64, #5907, #5191 ),
 .UNSPECIFIED., .F., .F.,
 ( 4, 2, 4 ),
 ( 0.002044882221487562268, 0.003063384235218290751, 0.004081886248949019233 ),
 .UNSPECIFIED. ) ;
#10134=VERTEX_POINT ( 'NONE', #4483 ) ;
#10154=DIRECTION ( 'NONE',  ( 0.000000000000000000, 0.000000000000000000, 1.000000000000000000 ) ) ;
#10158=VECTOR ( 'NONE', #255, 1000.000000000000000 ) ;
#10171=CARTESIAN_POINT ( 'NONE',  ( 3.170065989602867340, -3.373851915354596720, 1.156317065392270749 ) ) ;
#10179=ORIENTED_EDGE ( 'NONE', *, *, #7811, .F. ) ;
#10185=DIRECTION ( 'NONE',  ( 0.000000000000000000, -0.8660254037844317132, 0.5000000000000122125 ) ) ;
#10207=VECTOR ( 'NONE', #6622, 1000.000000000000000 ) ;
#10210=EDGE_LOOP ( 'NONE', ( #8054, #1578, #10545, #6455, #9354, #8155 ) ) ;
#10212=ORIENTED_EDGE ( 'NONE', *, *, #6691, .T. ) ;
#10230=VECTOR ( 'NONE', #1070, 999.9999999999998863 ) ;
#10244=SPHERICAL_SURFACE ( 'NONE', #7911, 3.250000000000000000 ) ;
#10247=EDGE_LOOP ( 'NONE', ( #2379, #5288, #9197, #1392, #5393, #8774 ) ) ;
#10256=SURFACE_SIDE_STYLE ('',( #6863 ) ) ;
#10257=DIRECTION ( 'NONE',  ( 1.000000000000000000, 0.000000000000000000, 0.000000000000000000 ) ) ;
#10283=B_SPLINE_CURVE_WITH_KNOTS ( 'NONE', 3,
 ( #1637, #9295, #10973, #2474 ),
 .UNSPECIFIED., .F., .F.,
 ( 4, 4 ),
 ( 2.380739282168294182E-07, 0.002044882221487568340 ),
 .UNSPECIFIED. ) ;
#10294=ADVANCED_FACE ( 'NONE', ( #556 ), #3074, .T. ) ;
#10319=EDGE_CURVE ( 'NONE', #3414, #783, #4071, .T. ) ;
#10330=VERTEX_POINT ( 'NONE', #8181 ) ;
#10333=VECTOR ( 'NONE', #1531, 1000.000000000000000 ) ;
#10335=FACE_OUTER_BOUND ( 'NONE', #10381, .T. ) ;
#10360=FACE_OUTER_BOUND ( 'NONE', #3446, .T. ) ;
#10363=FACE_OUTER_BOUND ( 'NONE', #3551, .T. ) ;
#10374=CIRCLE ( 'NONE', #7007, 0.1199999999999998845 ) ;
#10379=DIRECTION ( 'NONE',  ( -1.000000000000000000, -0.000000000000000000, -0.000000000000000000 ) ) ;
#10381=EDGE_LOOP ( 'NONE', ( #6213, #7404, #639, #10399 ) ) ;
#10383=CARTESIAN_POINT ( 'NONE',  ( 3.200000000000000178, 3.031088913245510774, -1.750000000000042411 ) ) ;
#10398=VECTOR ( 'NONE', #8881, 1000.000000000000000 ) ;
#10399=ORIENTED_EDGE ( 'NONE', *, *, #8723, .F. ) ;
#10408=FACE_OUTER_BOUND ( 'NONE', #8731, .T. ) ;
#10414=AXIS2_PLACEMENT_3D ( 'NONE', #2977, #6351, #395 ) ;
#10421=EDGE_CURVE ( 'NONE', #8739, #10063, #626, .T. ) ;
#10425=VERTEX_POINT ( 'NONE', #4121 ) ;
#10426=ADVANCED_FACE ( 'NONE', ( #5138 ), #1522, .T. ) ;
#10433=DIRECTION ( 'NONE',  ( 0.000000000000000000, 0.000000000000000000, -1.000000000000000000 ) ) ;
#10439=DIRECTION ( 'NONE',  ( 0.000000000000000000, 0.000000000000000000, -1.000000000000000000 ) ) ;
#10449=CARTESIAN_POINT ( 'NONE',  ( 0.3126073911696448659, -4.041451884327390331, 2.328673539876467720E-14 ) ) ;
#10468=DIRECTION ( 'NONE',  ( 0.000000000000000000, 0.000000000000000000, 1.000000000000000000 ) ) ;
#10474=CARTESIAN_POINT ( 'NONE',  ( 0.000000000000000000, 0.000000000000000000, 0.000000000000000000 ) ) ;
#10521=CARTESIAN_POINT ( 'NONE',  ( 0.000000000000000000, 0.000000000000000000, 0.000000000000000000 ) ) ;
#10525=CARTESIAN_POINT ( 'NONE',  ( 3.078243469714878167, 3.710888496608943488, 0.5725525826504455074 ) ) ;
#10527=DIRECTION ( 'NONE',  ( 0.000000000000000000, 0.000000000000000000, -1.000000000000000000 ) ) ;
#10539=CARTESIAN_POINT ( 'NONE',  ( 0.02539999999999975264, 0.000000000000000000, 0.000000000000000000 ) ) ;
#10545=ORIENTED_EDGE ( 'NONE', *, *, #9398, .F. ) ;
#10585=DIRECTION ( 'NONE',  ( 0.000000000000000000, 0.000000000000000000, 1.000000000000000000 ) ) ;
#10592=CARTESIAN_POINT ( 'NONE',  ( 0.1217565302851089937, -3.710888496608915510, 0.5725525826504929139 ) ) ;
#10599=LINE ( 'NONE', #201, #5897 ) ;
#10609=TOROIDAL_SURFACE ( 'NONE', #7231, 3.369999999999997886, 0.1199999999999999956 ) ;
#10616=EDGE_LOOP ( 'NONE', ( #4503, #10212, #9892 ) ) ;
#10620=ORIENTED_EDGE ( 'NONE', *, *, #1460, .F. ) ;
#10633=EDGE_LOOP ( 'NONE', ( #8827, #889 ) ) ;
#10635=ADVANCED_FACE ( 'NONE', ( #1343 ), #10609, .F. ) ;
#10636=B_SPLINE_CURVE_WITH_KNOTS ( 'NONE', 3,
 ( #6255, #2776, #9648, #2939 ),
 .UNSPECIFIED., .F., .F.,
 ( 4, 4 ),
 ( 2.380739282167226656E-07, 0.002044882221487536681 ),
 .UNSPECIFIED. ) ;
#10641=EDGE_CURVE ( 'NONE', #10050, #4107, #6673, .T. ) ;
#10661=CARTESIAN_POINT ( 'NONE',  ( 0.1388410611046147491, -3.710337782248049887, -0.5735064479039554408 ) ) ;
#10672=CARTESIAN_POINT ( 'NONE',  ( 0.02937408083519552765, -0.6808742863896954933, -3.499999999999999556 ) ) ;
#10693=CIRCLE ( 'NONE', #9808, 3.499999999999999556 ) ;
#10699=FACE_OUTER_BOUND ( 'NONE', #8971, .T. ) ;
#10702=DIRECTION ( 'NONE',  ( 1.000000000000000000, 0.000000000000000000, 0.000000000000000000 ) ) ;
#10731=CARTESIAN_POINT ( 'NONE',  ( 0.3126073911696528040, 2.020725942163738686, 3.499999999999999556 ) ) ;
#10745=LINE ( 'NONE', #5593, #10207 ) ;
#10746=EDGE_CURVE ( 'NONE', #8739, #3105, #3506, .T. ) ;
#10754=B_SPLINE_CURVE_WITH_KNOTS ( 'NONE', 3,
 ( #8537, #2658, #4488, #7872 ),
 .UNSPECIFIED., .F., .F.,
 ( 4, 4 ),
 ( 2.380739282167534764E-07, 0.002044882221487497216 ),
 .UNSPECIFIED. ) ;
#10761=( LENGTH_UNIT ( ) NAMED_UNIT ( * ) SI_UNIT ( .MILLI., .METRE. ) );
#10773=( LENGTH_UNIT ( ) NAMED_UNIT ( * ) SI_UNIT ( .MILLI., .METRE. ) );
#10812=CARTESIAN_POINT ( 'NONE',  ( 3.199999999999999734, -3.031088913245509886, 1.750000000000043077 ) ) ;
#10813=EDGE_CURVE ( 'NONE', #7419, #1521, #5099, .T. ) ;
#10814=ADVANCED_FACE ( 'NONE', ( #2557 ), #135, .T. ) ;
#10834=CARTESIAN_POINT ( 'NONE',  ( 0.3126073911691547025, -2.020725942164465661, -3.499999999999999556 ) ) ;
#10837=CARTESIAN_POINT ( 'NONE',  ( 3.200000000000000178, 4.041451884327400101, -2.303506639521620593E-14 ) ) ;
#10844=DIRECTION ( 'NONE',  ( -1.000000000000000000, -0.000000000000000000, -0.000000000000000000 ) ) ;
#10854=CARTESIAN_POINT ( 'NONE',  ( 0.000000000000000000, 0.000000000000000000, -3.499999999999999556 ) ) ;
#10873=DIRECTION ( 'NONE',  ( 0.000000000000000000, 0.000000000000000000, 1.000000000000000000 ) ) ;
#10875=VERTEX_POINT ( 'NONE', #7976 ) ;
#10915=DIRECTION ( 'NONE',  ( 0.000000000000000000, 0.000000000000000000, -1.000000000000000000 ) ) ;
#10936=FACE_OUTER_BOUND ( 'NONE', #5895, .T. ) ;
#10938=ORIENTED_EDGE ( 'NONE', *, *, #9812, .F. ) ;
#10942=DIRECTION ( 'NONE',  ( -1.000000000000000000, -0.000000000000000000, -0.000000000000000000 ) ) ;
#10948=ORIENTED_EDGE ( 'NONE', *, *, #8584, .T. ) ;
#10957=EDGE_CURVE ( 'NONE', #3329, #3105, #2869, .T. ) ;
#10959=AXIS2_PLACEMENT_3D ( 'NONE', #9930, #4878, #2366 ) ;
#10964=FACE_OUTER_BOUND ( 'NONE', #4809, .T. ) ;
#10967=ORIENTED_EDGE ( 'NONE', *, *, #5871, .T. ) ;
#10973=CARTESIAN_POINT ( 'NONE',  ( -1.917253639661504005E-15, 3.375361811986492988, -1.153701847711665618 ) ) ;
#10990=EDGE_CURVE ( 'NONE', #6272, #3329, #7399, .T. ) ;
ENDSEC;
END-ISO-10303-21;
